ISO-10303-21;
HEADER;
FILE_DESCRIPTION (('STEP AP214'),
    '1' );
FILE_NAME ('hex flange nut gradea_iso_ISO - 4161 - M5 - N.step',
    '2026-10-08T05:45:04',
    ( '' ),
    ( '' ),
    'SwSTEP 2.0',
    'SolidWorks 2026',
    '' );
FILE_SCHEMA (( 'AUTOMOTIVE_DESIGN' ));
ENDSEC;

DATA;
#4=B_SPLINE_CURVE_WITH_KNOTS ( 'NONE', 3,
 ( #2921, #5637, #7133, #6355, #5528 ),
 .UNSPECIFIED., .F., .F.,
 ( 4, 1, 4 ),
 ( 5.640274452250024914E-20, 0.002309401076758505356, 0.004618802153517010713 ),
 .UNSPECIFIED. ) ;
#12=VERTEX_POINT ( 'NONE', #2248 ) ;
#15=CONICAL_SURFACE ( 'NONE', #541, 4.000000000000000000, 0.8911886515913786111 ) ;
#16=CARTESIAN_POINT ( 'NONE',  ( -4.211405944401398038, -2.460460786169389902, -3.751298493805494072 ) ) ;
#38=VERTEX_POINT ( 'NONE', #5852 ) ;
#45=CARTESIAN_POINT ( 'NONE',  ( 2.449848172108560096, 3.432307619358740514, -3.503702292528905637 ) ) ;
#51=FACE_OUTER_BOUND ( 'NONE', #9561, .T. ) ;
#55=DIRECTION ( 'NONE',  ( -1.000000000000000000, 0.000000000000000000, 0.000000000000000000 ) ) ;
#56=ORIENTED_EDGE ( 'NONE', *, *, #4099, .F. ) ;
#69=CARTESIAN_POINT ( 'NONE',  ( -2.688821387764050996E-14, -4.618802153517012954, -0.4999999999999995559 ) ) ;
#76=CARTESIAN_POINT ( 'NONE',  ( 3.453038570460273071, 2.625189405340834448, -3.535263753543585352 ) ) ;
#104=VECTOR ( 'NONE', #726, 999.9999999999998863 ) ;
#115=EDGE_LOOP ( 'NONE', ( #4415, #1242, #292 ) ) ;
#138=CARTESIAN_POINT ( 'NONE',  ( 0.6810597143197052450, 4.461075778259290914, -3.598441714920602053 ) ) ;
#142=CARTESIAN_POINT ( 'NONE',  ( 3.680118525130245732, -2.494084732383344605, -0.3507732604232533524 ) ) ;
#144=CIRCLE ( 'NONE', #7774, 5.560781378645573980 ) ;
#159=CARTESIAN_POINT ( 'NONE',  ( -4.000000000000000000, 0.000000000000000000, 0.000000000000000000 ) ) ;
#166=CARTESIAN_POINT ( 'NONE',  ( -3.349226789952655547, -2.685125164760744809, -0.2236248678334863682 ) ) ;
#170=VERTEX_POINT ( 'NONE', #8523 ) ;
#171=DIRECTION ( 'NONE',  ( 1.000000000000000000, 0.000000000000000000, 0.000000000000000000 ) ) ;
#184=ORIENTED_EDGE ( 'NONE', *, *, #1115, .T. ) ;
#192=EDGE_CURVE ( 'NONE', #5966, #5040, #1802, .T. ) ;
#225=EDGE_CURVE ( 'NONE', #3283, #7506, #8145, .T. ) ;
#237=LINE ( 'NONE', #3635, #4176 ) ;
#245=CARTESIAN_POINT ( 'NONE',  ( 4.000000000000000000, -2.309401076758516691, -0.4999999999999995559 ) ) ;
#258=EDGE_LOOP ( 'NONE', ( #649, #8272, #6684, #10787 ) ) ;
#292=ORIENTED_EDGE ( 'NONE', *, *, #3597, .F. ) ;
#304=LINE ( 'NONE', #1193, #3144 ) ;
#307=( GEOMETRIC_REPRESENTATION_CONTEXT ( 3 ) GLOBAL_UNCERTAINTY_ASSIGNED_CONTEXT ( ( #7294 ) ) GLOBAL_UNIT_ASSIGNED_CONTEXT ( ( #5535, #3754, #8140 ) ) REPRESENTATION_CONTEXT ( 'NONE', 'WORKASPACE' ) );
#308=AXIS2_PLACEMENT_3D ( 'NONE', #6956, #4296, #9565 ) ;
#309=CARTESIAN_POINT ( 'NONE',  ( 4.197393957002303999, 7.772902908466098641E-14, -3.503767560748929810 ) ) ;
#316=CARTESIAN_POINT ( 'NONE',  ( 0.000000000000000000, 0.000000000000000000, -4.484454397937119197 ) ) ;
#324=CARTESIAN_POINT ( 'NONE',  ( -2.000000000000002665, -3.464101615137770374, -3.142992957459237680 ) ) ;
#349=CARTESIAN_POINT ( 'NONE',  ( 0.000000000000000000, 0.000000000000000000, 0.000000000000000000 ) ) ;
#393=ORIENTED_EDGE ( 'NONE', *, *, #3763, .T. ) ;
#412=CARTESIAN_POINT ( 'NONE',  ( -4.236525694536558362, 2.416953475386465211, -3.751298745799836354 ) ) ;
#416=ORIENTED_EDGE ( 'NONE', *, *, #2889, .T. ) ;
#417=CARTESIAN_POINT ( 'NONE',  ( -1.312671235360383548, -3.860931062424228788, -0.05923475698271369466 ) ) ;
#430=B_SPLINE_CURVE_WITH_KNOTS ( 'NONE', 3,
 ( #3945, #1448, #2175, #4061, #499, #4743 ),
 .UNSPECIFIED., .F., .F.,
 ( 4, 2, 4 ),
 ( 0.000000000000000000, 0.0002095117440854730670, 0.0004190234881709461339 ),
 .UNSPECIFIED. ) ;
#435=ORIENTED_EDGE ( 'NONE', *, *, #8120, .F. ) ;
#441=EDGE_CURVE ( 'NONE', #38, #9170, #10272, .T. ) ;
#445=CARTESIAN_POINT ( 'NONE',  ( -4.024497503033519941, 2.323544716729375459, -3.572167766733379768 ) ) ;
#471=B_SPLINE_CURVE_WITH_KNOTS ( 'NONE', 3,
 ( #1292, #9621, #2745, #445, #3626, #7912 ),
 .UNSPECIFIED., .F., .F.,
 ( 4, 2, 4 ),
 ( -3.640115492410698714E-06, 0.0002066546034006521879, 0.0004169493222937151081 ),
 .UNSPECIFIED. ) ;
#475=VECTOR ( 'NONE', #4688, 1000.000000000000000 ) ;
#490=CARTESIAN_POINT ( 'NONE',  ( -1.391697335622809950, -4.043246145443391448, -3.503898532754372575 ) ) ;
#493=PLANE ( 'NONE',  #6999 ) ;
#499=CARTESIAN_POINT ( 'NONE',  ( 4.154306624731137099, 2.398490048084935822, -3.721999068284414847 ) ) ;
#538=CARTESIAN_POINT ( 'NONE',  ( -6.473970235329672780E-16, -4.862606272033106691, -3.745885042887442395 ) ) ;
#541=AXIS2_PLACEMENT_3D ( 'NONE', #3800, #8078, #5529 ) ;
#557=CARTESIAN_POINT ( 'NONE',  ( -6.259644161404862988E-16, -4.618802153517027165, -3.504271511726793076 ) ) ;
#560=CARTESIAN_POINT ( 'NONE',  ( 4.000000000000000000, 0.9868501483902631932, -0.09357334158579604100 ) ) ;
#562=CARTESIAN_POINT ( 'NONE',  ( -1.747541505913277282, 3.837784562140256650, -3.503702292528906526 ) ) ;
#572=EDGE_CURVE ( 'NONE', #1489, #6302, #6943, .T. ) ;
#579=CARTESIAN_POINT ( 'NONE',  ( -2.000000000000007550, -3.464101615137749945, 0.000000000000000000 ) ) ;
#581=ADVANCED_FACE ( 'NONE', ( #765 ), #3396, .T. ) ;
#596=ORIENTED_EDGE ( 'NONE', *, *, #6379, .F. ) ;
#620=CARTESIAN_POINT ( 'NONE',  ( -5.384454397937118664, 6.594054843588581554E-16, -4.484454397937119197 ) ) ;
#636=CARTESIAN_POINT ( 'NONE',  ( -6.473970235329672780E-16, -4.862606272033106691, -3.745885042887442395 ) ) ;
#649=ORIENTED_EDGE ( 'NONE', *, *, #10640, .T. ) ;
#660=CARTESIAN_POINT ( 'NONE',  ( -4.211140560182196957, -2.431303136016552013, -3.745885042887436178 ) ) ;
#676=CARTESIAN_POINT ( 'NONE',  ( -0.3208286057739654917, 4.433571671609680465, -0.3503314178412548774 ) ) ;
#688=CARTESIAN_POINT ( 'NONE',  ( 1.144235203016666258, 3.958177651039090250, -0.09382832055445661235 ) ) ;
#689=CARTESIAN_POINT ( 'NONE',  ( 4.000000000000000000, -2.471525695159793035, -3.686886880705770864 ) ) ;
#693=EDGE_CURVE ( 'NONE', #4635, #7216, #8152, .T. ) ;
#709=ADVANCED_FACE ( 'NONE', ( #6106 ), #741, .T. ) ;
#726=DIRECTION ( 'NONE',  ( -0.8191520442889875797, 1.003171929053519570E-16, 0.5735764363510522656 ) ) ;
#728=DIRECTION ( 'NONE',  ( 0.5000000000000022204, 0.8660254037844374864, -0.000000000000000000 ) ) ;
#729=ORIENTED_EDGE ( 'NONE', *, *, #4099, .T. ) ;
#732=CARTESIAN_POINT ( 'NONE',  ( -4.000000000000000000, -2.512220745329312610, -3.469390707569719901 ) ) ;
#734=CARTESIAN_POINT ( 'NONE',  ( 4.197393957002303999, 0.8151795401431359833, -3.503767560748935139 ) ) ;
#741=CONICAL_SURFACE ( 'NONE', #3236, 4.000000000000000000, 0.8911886515913786111 ) ;
#756=ORIENTED_EDGE ( 'NONE', *, *, #4402, .T. ) ;
#765=FACE_OUTER_BOUND ( 'NONE', #10921, .T. ) ;
#805=B_SPLINE_CURVE_WITH_KNOTS ( 'NONE', 3,
 ( #2324, #1391, #1333, #3057, #5717, #7489 ),
 .UNSPECIFIED., .F., .F.,
 ( 4, 2, 4 ),
 ( 4.336808689942017736E-19, 0.0002095117440854729585, 0.0004190234881709454834 ),
 .UNSPECIFIED. ) ;
#806=B_SPLINE_CURVE_WITH_KNOTS ( 'NONE', 3,
 ( #4263, #5098, #3194, #3311, #7648, #10148 ),
 .UNSPECIFIED., .F., .F.,
 ( 4, 2, 4 ),
 ( 0.002365888236227995517, 0.003551327329835084114, 0.004736766423442172712 ),
 .UNSPECIFIED. ) ;
#813=ORIENTED_EDGE ( 'NONE', *, *, #5057, .F. ) ;
#840=DIRECTION ( 'NONE',  ( 0.000000000000000000, 0.000000000000000000, -1.000000000000000000 ) ) ;
#843=DIRECTION ( 'NONE',  ( 0.8660254037844374864, -0.5000000000000018874, 0.000000000000000000 ) ) ;
#864=CARTESIAN_POINT ( 'NONE',  ( -4.203833317240879275, -1.627343821129593859, -3.597273115243890818 ) ) ;
#878=DIRECTION ( 'NONE',  ( 1.000000000000000000, 0.000000000000000000, 0.000000000000000000 ) ) ;
#892=EDGE_CURVE ( 'NONE', #7431, #6444, #4678, .T. ) ;
#903=ORIENTED_EDGE ( 'NONE', *, *, #7998, .F. ) ;
#907=FACE_OUTER_BOUND ( 'NONE', #4689, .T. ) ;
#933=B_SPLINE_CURVE_WITH_KNOTS ( 'NONE', 3,
 ( #5260, #6137, #1814, #4375, #6864, #9529 ),
 .UNSPECIFIED., .F., .F.,
 ( 4, 2, 4 ),
 ( -3.640115492407174633E-06, 0.0002066546034006553863, 0.0004169493222937179812 ),
 .UNSPECIFIED. ) ;
#936=CARTESIAN_POINT ( 'NONE',  ( -5.560781378645573980, 0.000000000000000000, -4.000000000000000000 ) ) ;
#961=DIRECTION ( 'NONE',  ( -1.000000000000000000, 0.000000000000000000, 0.000000000000000000 ) ) ;
#963=CONICAL_SURFACE ( 'NONE', #7532, 4.000000000000000000, 0.8911886515913786111 ) ;
#965=FACE_OUTER_BOUND ( 'NONE', #258, .T. ) ;
#976=CARTESIAN_POINT ( 'NONE',  ( -3.333333333333335258, 2.694301256218251783, -3.300726591567079815 ) ) ;
#985=CIRCLE ( 'NONE', #10037, 4.000000000000000000 ) ;
#987=ORIENTED_EDGE ( 'NONE', *, *, #1068, .F. ) ;
#990=VERTEX_POINT ( 'NONE', #3562 ) ;
#999=CARTESIAN_POINT ( 'NONE',  ( 0.000000000000000000, 0.000000000000000000, -4.974599999999998801 ) ) ;
#1025=CARTESIAN_POINT ( 'NONE',  ( 0.000000000000000000, 0.000000000000000000, 0.000000000000000000 ) ) ;
#1035=AXIS2_PLACEMENT_3D ( 'NONE', #10048, #7874, #4440 ) ;
#1068=EDGE_CURVE ( 'NONE', #8576, #3283, #3437, .T. ) ;
#1079=ORIENTED_EDGE ( 'NONE', *, *, #1783, .T. ) ;
#1080=B_SPLINE_CURVE_WITH_KNOTS ( 'NONE', 3,
 ( #5653, #8197, #8249, #1587, #5596, #2311, #6574, #636 ),
 .UNSPECIFIED., .F., .F.,
 ( 4, 2, 2, 4 ),
 ( 0.000000000000000000, 0.002450665683189819262, 0.003675998524784728893, 0.004901331366379639391 ),
 .UNSPECIFIED. ) ;
#1087=CONICAL_SURFACE ( 'NONE', #6767, 4.000000000000000000, 0.8911886515913786111 ) ;
#1090=B_SPLINE_CURVE_WITH_KNOTS ( 'NONE', 3,
 ( #5226, #10277, #8608, #45, #6100, #3503, #2618, #7786 ),
 .UNSPECIFIED., .F., .F.,
 ( 4, 2, 2, 4 ),
 ( 7.780516681398759253E-20, 0.002450665683189819696, 0.003675998524784729327, 0.004901331366379639391 ),
 .UNSPECIFIED. ) ;
#1096=PRODUCT_CONTEXT ( 'NONE', #9837, 'mechanical' ) ;
#1100=AXIS2_PLACEMENT_3D ( 'NONE', #6812, #5163, #9482 ) ;
#1115=EDGE_CURVE ( 'NONE', #7952, #8322, #1825, .T. ) ;
#1125=CARTESIAN_POINT ( 'NONE',  ( 1.567478505476134606E-15, 4.618802153517012066, -3.433295621305382905 ) ) ;
#1128=FACE_OUTER_BOUND ( 'NONE', #115, .T. ) ;
#1140=CONICAL_SURFACE ( 'NONE', #4151, 2.059999999999998721, 0.9599310885968738161 ) ;
#1146=ORIENTED_EDGE ( 'NONE', *, *, #9929, .F. ) ;
#1152=DIRECTION ( 'NONE',  ( 0.8191520442889875797, 0.000000000000000000, 0.5735764363510522656 ) ) ;
#1162=AXIS2_PLACEMENT_3D ( 'NONE', #6518, #2357, #3138 ) ;
#1176=CARTESIAN_POINT ( 'NONE',  ( -2.171643655288372443, 3.365003104552320767, 2.541098841762897165E-18 ) ) ;
#1177=LINE ( 'NONE', #3685, #475 ) ;
#1193=CARTESIAN_POINT ( 'NONE',  ( -2.500000000000000444, 3.061616997868383634E-16, -25.03750572909317285 ) ) ;
#1205=( BOUNDED_SURFACE ( )  B_SPLINE_SURFACE ( 3, 2, ( 
 ( #2534, #689, #8415 ),
 ( #7530, #9195, #4088 ),
 ( #2598, #9976, #7418 ),
 ( #2362, #9247, #4203 ),
 ( #5977, #1477, #5807 ),
 ( #4872, #8250, #9136 ) ),
 .UNSPECIFIED., .F., .F., .F. ) 
 B_SPLINE_SURFACE_WITH_KNOTS ( ( 4, 2, 4 ),
 ( 3, 3 ),
 ( 0.02027065861071770947, 0.02273072267836921331, 0.02519078674602071716 ),
 ( 0.000000000000000000, 1.000000000000000000 ),
 .UNSPECIFIED. ) 
 GEOMETRIC_REPRESENTATION_ITEM ( )  RATIONAL_B_SPLINE_SURFACE ( (
 ( 1.000000000000000000, 0.8047781708337304885, 1.000000000000000000),
 ( 1.000000000000000000, 0.8123765190705307671, 1.000000000000000000),
 ( 1.000000000000000000, 0.8190656277163975707, 1.000000000000000000),
 ( 1.000000000000000000, 0.8192366903512159348, 1.000000000000000000),
 ( 1.000000000000000000, 0.8126138454302893610, 1.000000000000000000),
 ( 1.000000000000000000, 0.8047712246031417660, 1.000000000000000000) ) ) 
 REPRESENTATION_ITEM ( '' )  SURFACE ( )  );
#1219=B_SPLINE_CURVE_WITH_KNOTS ( 'NONE', 3,
 ( #6796, #7640, #1523, #8351, #5856, #69 ),
 .UNSPECIFIED., .F., .F.,
 ( 4, 2, 4 ),
 ( 0.002365888236227967761, 0.003551327329835077609, 0.004736766423442186590 ),
 .UNSPECIFIED. ) ;
#1221=AXIS2_PLACEMENT_3D ( 'NONE', #3907, #4755, #9632 ) ;
#1242=ORIENTED_EDGE ( 'NONE', *, *, #3599, .T. ) ;
#1267=AXIS2_PLACEMENT_3D ( 'NONE', #2514, #2401, #843 ) ;
#1268=ORIENTED_EDGE ( 'NONE', *, *, #892, .T. ) ;
#1285=ORIENTED_EDGE ( 'NONE', *, *, #8430, .T. ) ;
#1290=CARTESIAN_POINT ( 'NONE',  ( -4.000000000000000888, -2.309401076758512694, -3.504269196027526512 ) ) ;
#1292=CARTESIAN_POINT ( 'NONE',  ( -4.211140560182196957, 2.431303136016537803, -3.745885042887433514 ) ) ;
#1293=CARTESIAN_POINT ( 'NONE',  ( -2.000000000000006661, 3.464101615137750834, 0.000000000000000000 ) ) ;
#1299=CARTESIAN_POINT ( 'NONE',  ( -4.000000000000000000, 1.941961291383472732, -0.3515519931180205448 ) ) ;
#1316=CARTESIAN_POINT ( 'NONE',  ( -3.472371940586054251, -2.614027278893156669, -3.320322319202162031 ) ) ;
#1332=ORIENTED_EDGE ( 'NONE', *, *, #10711, .F. ) ;
#1333=CARTESIAN_POINT ( 'NONE',  ( 4.024499207728657879, -2.323545700935587988, -3.572172305156509964 ) ) ;
#1345=B_SPLINE_CURVE_WITH_KNOTS ( 'NONE', 3,
 ( #7291, #5011, #1668, #6404, #560, #9801, #9275, #10642 ),
 .UNSPECIFIED., .F., .F.,
 ( 4, 2, 2, 4 ),
 ( 0.005725059856848645212, 0.006314084072593634418, 0.006903108288338624492, 0.008081156719828603771 ),
 .UNSPECIFIED. ) ;
#1366=CARTESIAN_POINT ( 'NONE',  ( -4.000000000000000000, 1.700094919196744270, -3.320312364301766017 ) ) ;
#1367=COLOUR_RGB ( '', 0.09019608, 0.27058824, 0.51372549) ;
#1370=CARTESIAN_POINT ( 'NONE',  ( -1.257172072275743346, 3.892973519171203378, -3.433252694550776862 ) ) ;
#1377=DIRECTION ( 'NONE',  ( -0.000000000000000000, -0.000000000000000000, 1.000000000000000000 ) ) ;
#1391=CARTESIAN_POINT ( 'NONE',  ( 4.000000000000003553, -2.309401076758513138, -3.504271511726786859 ) ) ;
#1400=FACE_OUTER_BOUND ( 'NONE', #10325, .T. ) ;
#1419=VERTEX_POINT ( 'NONE', #8880 ) ;
#1421=DIRECTION ( 'NONE',  ( 1.000000000000000000, 0.000000000000000000, 0.000000000000000000 ) ) ;
#1423=CARTESIAN_POINT ( 'NONE',  ( 4.197393957002303999, 7.772902908466098641E-14, -3.503767560748929810 ) ) ;
#1424=CARTESIAN_POINT ( 'NONE',  ( -1.360585162435467455, 4.061296242128285883, -3.505054077164959203 ) ) ;
#1427=CARTESIAN_POINT ( 'NONE',  ( 0.1410422978106145031, -4.700232962125109104, -3.687027686973628704 ) ) ;
#1441=ORIENTED_EDGE ( 'NONE', *, *, #5196, .T. ) ;
#1444=VECTOR ( 'NONE', #10419, 1000.000000000000000 ) ;
#1448=CARTESIAN_POINT ( 'NONE',  ( 3.999999999999999112, 2.309401076758497595, -3.504271511726784194 ) ) ;
#1458=EDGE_CURVE ( 'NONE', #10907, #3061, #1080, .T. ) ;
#1466=CARTESIAN_POINT ( 'NONE',  ( -2.059999999999998721, 2.522772406243545965E-16, -0.3080913168122742518 ) ) ;
#1477=CARTESIAN_POINT ( 'NONE',  ( 4.000000000001088907, 1.658577278524410170, -3.531553309554541720 ) ) ;
#1489=VERTEX_POINT ( 'NONE', #4933 ) ;
#1497=CARTESIAN_POINT ( 'NONE',  ( 0.000000000000000000, 0.000000000000000000, -4.694516984716113228 ) ) ;
#1498=AXIS2_PLACEMENT_3D ( 'NONE', #4277, #6937, #2614 ) ;
#1499=CARTESIAN_POINT ( 'NONE',  ( 1.243802165048773611, -3.900692638707475624, -3.223146290109810241 ) ) ;
#1511=FACE_OUTER_BOUND ( 'NONE', #6548, .T. ) ;
#1523=CARTESIAN_POINT ( 'NONE',  ( 1.317756351988342622, -3.857995168970215438, -0.04852650426602527628 ) ) ;
#1534=ORIENTED_EDGE ( 'NONE', *, *, #4741, .F. ) ;
#1547=EDGE_LOOP ( 'NONE', ( #5224, #6437, #4786, #1754 ) ) ;
#1561=CARTESIAN_POINT ( 'NONE',  ( -4.211140560182196957, 2.431303136016537803, -3.745885042887433514 ) ) ;
#1583=EDGE_CURVE ( 'NONE', #4391, #10481, #4406, .T. ) ;
#1587=CARTESIAN_POINT ( 'NONE',  ( 1.747541505913279281, -3.837784562140273081, -3.503702292528912299 ) ) ;
#1629=CARTESIAN_POINT ( 'NONE',  ( 0.000000000000000000, 0.000000000000000000, -0.2800830152838844622 ) ) ;
#1651=DIRECTION ( 'NONE',  ( 0.000000000000000000, 0.000000000000000000, 1.000000000000000000 ) ) ;
#1659=ORIENTED_EDGE ( 'NONE', *, *, #8430, .F. ) ;
#1668=CARTESIAN_POINT ( 'NONE',  ( 4.000000000000000000, 0.3987449864460005378, -0.01220643443059817035 ) ) ;
#1673=ORIENTED_EDGE ( 'NONE', *, *, #2965, .T. ) ;
#1688=EDGE_LOOP ( 'NONE', ( #8283, #1534, #3204, #10954, #9953 ) ) ;
#1712=ORIENTED_EDGE ( 'NONE', *, *, #5400, .T. ) ;
#1717=VERTEX_POINT ( 'NONE', #8358 ) ;
#1719=ORIENTED_EDGE ( 'NONE', *, *, #3774, .T. ) ;
#1728=B_SPLINE_CURVE_WITH_KNOTS ( 'NONE', 3,
 ( #2309, #4026, #5700, #4198, #6572 ),
 .UNSPECIFIED., .F., .F.,
 ( 4, 1, 4 ),
 ( 0.000000000000000000, 0.002309401076758505790, 0.004618802153517011580 ),
 .UNSPECIFIED. ) ;
#1735=CIRCLE ( 'NONE', #10951, 4.000000000000000000 ) ;
#1754=ORIENTED_EDGE ( 'NONE', *, *, #10410, .F. ) ;
#1768=CARTESIAN_POINT ( 'NONE',  ( 1.567478505476134606E-15, 4.618802153517012066, -3.433295621305382905 ) ) ;
#1778=DIRECTION ( 'NONE',  ( -0.000000000000000000, -0.000000000000000000, 1.000000000000000000 ) ) ;
#1783=EDGE_CURVE ( 'NONE', #8322, #7952, #9375, .T. ) ;
#1784=DIRECTION ( 'NONE',  ( 0.000000000000000000, 0.000000000000000000, -1.000000000000000000 ) ) ;
#1802=LINE ( 'NONE', #5519, #9494 ) ;
#1808=CARTESIAN_POINT ( 'NONE',  ( 1.734723475976807094E-15, 4.618802153517012954, -0.4999999999999995559 ) ) ;
#1809=CARTESIAN_POINT ( 'NONE',  ( -4.000000000000000000, -2.472261339043343220, -3.687027428081192326 ) ) ;
#1810=CARTESIAN_POINT ( 'NONE',  ( -2.688821387764050996E-14, -4.618802153517012954, -0.4999999999999995559 ) ) ;
#1814=CARTESIAN_POINT ( 'NONE',  ( 2.548804901056335857E-15, 4.736522675502163437, -3.681124513963624612 ) ) ;
#1819=CARTESIAN_POINT ( 'NONE',  ( -0.6666666666666651864, 4.233901974057260098, -3.300726591567081147 ) ) ;
#1825=CIRCLE ( 'NONE', #1100, 2.500000000000000444 ) ;
#1839=CARTESIAN_POINT ( 'NONE',  ( -4.000000000000000000, 2.309401076758498483, -5.000000000000000000 ) ) ;
#1867=CARTESIAN_POINT ( 'NONE',  ( 2.855764796983346177, -2.970025579236428737, -0.09382832055446485575 ) ) ;
#1868=ORIENTED_EDGE ( 'NONE', *, *, #3317, .T. ) ;
#1873=CARTESIAN_POINT ( 'NONE',  ( 4.211140560182196957, -2.431303136016555122, -3.745885042887436622 ) ) ;
#1874=( BOUNDED_SURFACE ( )  B_SPLINE_SURFACE ( 3, 2, ( 
 ( #4842, #8216, #5570 ),
 ( #2287, #9948, #7387 ),
 ( #1499, #3064, #8898 ),
 ( #3842, #5675, #4900 ),
 ( #8169, #6393, #3997 ),
 ( #10778, #3167, #9053 ) ),
 .UNSPECIFIED., .F., .F., .F. ) 
 B_SPLINE_SURFACE_WITH_KNOTS ( ( 4, 2, 4 ),
 ( 3, 3 ),
 ( 0.02032853247518126918, 0.02278863295364821906, 0.02524873343211517240 ),
 ( 0.000000000000000000, 1.000000000000000000 ),
 .UNSPECIFIED. ) 
 GEOMETRIC_REPRESENTATION_ITEM ( )  RATIONAL_B_SPLINE_SURFACE ( (
 ( 1.000000000000000000, 0.8047781615896837382, 1.000000000000000000),
 ( 1.000000000000000000, 0.8123767586289252218, 1.000000000000000000),
 ( 1.000000000000000000, 0.8190662415564388121, 1.000000000000000000),
 ( 1.000000000000000000, 0.8192361015669026303, 1.000000000000000000),
 ( 1.000000000000000000, 0.8126135807103900266, 1.000000000000000000),
 ( 1.000000000000000000, 0.8047712338318593339, 1.000000000000000000) ) ) 
 REPRESENTATION_ITEM ( '' )  SURFACE ( )  );
#1875=UNCERTAINTY_MEASURE_WITH_UNIT (LENGTH_MEASURE( 1.000000000000000082E-05 ), #4788, 'distance_accuracy_value', 'NONE');
#1876=AXIS2_PLACEMENT_3D ( 'NONE', #8470, #8578, #961 ) ;
#1888=EDGE_CURVE ( 'NONE', #9170, #5606, #1345, .T. ) ;
#1889=FACE_OUTER_BOUND ( 'NONE', #6739, .T. ) ;
#1924=EDGE_CURVE ( 'NONE', #7431, #7847, #4956, .T. ) ;
#1926=CARTESIAN_POINT ( 'NONE',  ( 3.540020015735602765, 2.810662092924382627, -3.602146406945867962 ) ) ;
#1943=FACE_OUTER_BOUND ( 'NONE', #9037, .T. ) ;
#1981=ORIENTED_EDGE ( 'NONE', *, *, #5666, .F. ) ;
#1986=FACE_OUTER_BOUND ( 'NONE', #10458, .T. ) ;
#1998=CARTESIAN_POINT ( 'NONE',  ( 4.000000000000000000, 2.309401076758497151, -3.433295621305379353 ) ) ;
#2001=ADVANCED_FACE ( 'NONE', ( #3858, #51 ), #5945, .F. ) ;
#2003=EDGE_CURVE ( 'NONE', #4635, #3058, #8504, .T. ) ;
#2006=B_SPLINE_CURVE_WITH_KNOTS ( 'NONE', 3,
 ( #538, #6588, #490, #2221, #5768, #3938, #7324, #9153 ),
 .UNSPECIFIED., .F., .F.,
 ( 4, 2, 2, 4 ),
 ( 0.000000000000000000, 0.002450665683189818828, 0.003675998524784728459, 0.004901331366379638524 ),
 .UNSPECIFIED. ) ;
#2009=ORIENTED_EDGE ( 'NONE', *, *, #1458, .F. ) ;
#2029=CARTESIAN_POINT ( 'NONE',  ( -0.3461262719736137305, 4.658553426539289610, -3.671615880910373608 ) ) ;
#2031=EDGE_CURVE ( 'NONE', #9170, #10481, #7798, .T. ) ;
#2032=ORIENTED_EDGE ( 'NONE', *, *, #1115, .F. ) ;
#2035=CARTESIAN_POINT ( 'NONE',  ( 4.207491450040567571, -2.029819825146485179, -3.671670828759567407 ) ) ;
#2039=CARTESIAN_POINT ( 'NONE',  ( -4.000000000000000000, -0.3979232138631226823, -3.896351557369779711E-17 ) ) ;
#2040=CARTESIAN_POINT ( 'NONE',  ( -2.807080416178626692, 3.225969019225154444, -3.502507215260441065 ) ) ;
#2051=ORIENTED_EDGE ( 'NONE', *, *, #3763, .F. ) ;
#2080=EDGE_CURVE ( 'NONE', #7845, #9793, #4, .T. ) ;
#2101=CARTESIAN_POINT ( 'NONE',  ( -3.522875095019672109, 2.820352903225427532, -3.598441714920591394 ) ) ;
#2111=CARTESIAN_POINT ( 'NONE',  ( -2.500000000000000444, 3.061616997868383634E-16, -5.000000000000000888 ) ) ;
#2125=SURFACE_SIDE_STYLE ('',( #4736 ) ) ;
#2129=CARTESIAN_POINT ( 'NONE',  ( -4.024497503033519941, -2.323544716729390558, -3.572167766733381544 ) ) ;
#2144=EDGE_CURVE ( 'NONE', #7845, #3061, #8754, .T. ) ;
#2145=ORIENTED_EDGE ( 'NONE', *, *, #6147, .T. ) ;
#2146=FILL_AREA_STYLE ('',( #5824 ) ) ;
#2162=CIRCLE ( 'NONE', #8360, 2.100000000000000089 ) ;
#2172=ORIENTED_EDGE ( 'NONE', *, *, #1783, .F. ) ;
#2175=CARTESIAN_POINT ( 'NONE',  ( 4.024499207728657879, 2.323545700935571556, -3.572172305156506411 ) ) ;
#2186=DIRECTION ( 'NONE',  ( 0.000000000000000000, 0.000000000000000000, -1.000000000000000000 ) ) ;
#2202=CARTESIAN_POINT ( 'NONE',  ( 1.654252653721905331, 3.663718938583014229, -0.01223254789873410957 ) ) ;
#2209=CIRCLE ( 'NONE', #1498, 5.384454397937118664 ) ;
#2221=CARTESIAN_POINT ( 'NONE',  ( -2.449848172108560540, -3.432307619358754724, -3.503702292528910078 ) ) ;
#2224=PRESENTATION_STYLE_ASSIGNMENT (( #4679 ) ) ;
#2248=CARTESIAN_POINT ( 'NONE',  ( 1.411581201560190495E-15, 4.862606272033091592, -3.745885042887436622 ) ) ;
#2249=DIRECTION ( 'NONE',  ( -1.000000000000000000, 0.000000000000000000, 0.000000000000000000 ) ) ;
#2260=CARTESIAN_POINT ( 'NONE',  ( -0.5449313310646672903, -4.304185902836978883, -3.316620875263469159 ) ) ;
#2262=AXIS2_PLACEMENT_3D ( 'NONE', #9122, #728, #8293 ) ;
#2264=DIRECTION ( 'NONE',  ( 0.000000000000000000, 0.000000000000000000, -1.000000000000000000 ) ) ;
#2265=CARTESIAN_POINT ( 'NONE',  ( -1.828356344711647319, -3.563200125723192002, -1.076197711133951296E-14 ) ) ;
#2266=ADVANCED_FACE ( 'NONE', ( #6506 ), #7571, .T. ) ;
#2287=CARTESIAN_POINT ( 'NONE',  ( 0.5276280594147412240, -4.314175951381924889, -3.320322319201654881 ) ) ;
#2290=CARTESIAN_POINT ( 'NONE',  ( 4.000000000000000000, -1.560351142792952617, -0.2242961665059816367 ) ) ;
#2309=CARTESIAN_POINT ( 'NONE',  ( 4.000000000000000000, -2.309401076758514915, -3.433295621305383349 ) ) ;
#2311=CARTESIAN_POINT ( 'NONE',  ( 0.6937372685066666156, -4.453844082567737672, -3.610536846335894445 ) ) ;
#2324=CARTESIAN_POINT ( 'NONE',  ( 4.000000000000000000, -2.309401076758514915, -3.433295621305383349 ) ) ;
#2326=DIRECTION ( 'NONE',  ( -0.8660254037844377084, -0.5000000000000015543, 0.000000000000000000 ) ) ;
#2353=EDGE_LOOP ( 'NONE', ( #813, #1285, #3939, #4050, #1268 ) ) ;
#2357=DIRECTION ( 'NONE',  ( -0.000000000000000000, 0.000000000000000000, -1.000000000000000000 ) ) ;
#2362=CARTESIAN_POINT ( 'NONE',  ( 4.000000000000000000, 0.8378280264232961239, -3.220590601395640018 ) ) ;
#2388=CIRCLE ( 'NONE', #2941, 2.100000000000000089 ) ;
#2389=CARTESIAN_POINT ( 'NONE',  ( 4.000000000000000000, 0.000000000000000000, 0.000000000000000000 ) ) ;
#2396=EDGE_CURVE ( 'NONE', #6934, #7320, #10806, .T. ) ;
#2401=DIRECTION ( 'NONE',  ( -0.5000000000000019984, -0.8660254037844375974, 0.000000000000000000 ) ) ;
#2413=B_SPLINE_CURVE_WITH_KNOTS ( 'NONE', 3,
 ( #3775, #8770, #324, #7157, #7890 ),
 .UNSPECIFIED., .F., .F.,
 ( 4, 1, 4 ),
 ( 0.000000000000000000, 0.002309401076758505356, 0.004618802153517010713 ),
 .UNSPECIFIED. ) ;
#2426=DIRECTION ( 'NONE',  ( 0.000000000000000000, 0.000000000000000000, 1.000000000000000000 ) ) ;
#2430=VECTOR ( 'NONE', #4581, 1000.000000000000000 ) ;
#2454=CARTESIAN_POINT ( 'NONE',  ( -4.197393957002303999, 0.4069871074557429025, -3.503767560748926257 ) ) ;
#2477=EDGE_CURVE ( 'NONE', #9793, #4773, #1728, .T. ) ;
#2485=CARTESIAN_POINT ( 'NONE',  ( -4.000000000000000000, 2.309401076758498483, -3.433295621305379353 ) ) ;
#2506=ORIENTED_EDGE ( 'NONE', *, *, #2144, .T. ) ;
#2514=CARTESIAN_POINT ( 'NONE',  ( -4.000000000000000000, -2.309401076758512694, -5.000000000000000000 ) ) ;
#2521=ORIENTED_EDGE ( 'NONE', *, *, #192, .F. ) ;
#2523=CARTESIAN_POINT ( 'NONE',  ( -4.000000000000000000, -7.806255641895631925E-15, -3.142992957459232350 ) ) ;
#2534=CARTESIAN_POINT ( 'NONE',  ( 4.000000000000000000, -2.511475576507276042, -3.469253905236643565 ) ) ;
#2541=LINE ( 'NONE', #4385, #9312 ) ;
#2555=B_SPLINE_CURVE_WITH_KNOTS ( 'NONE', 3,
 ( #2985, #5482, #5584, #562, #3751, #4596, #2029, #7137 ),
 .UNSPECIFIED., .F., .F.,
 ( 4, 2, 2, 4 ),
 ( 0.000000000000000000, 0.002450665683189820997, 0.003675998524784731495, 0.004901331366379641993 ),
 .UNSPECIFIED. ) ;
#2559=EDGE_CURVE ( 'NONE', #7845, #8932, #5973, .T. ) ;
#2564=DIRECTION ( 'NONE',  ( -1.000000000000000000, 0.000000000000000000, 0.000000000000000000 ) ) ;
#2573=ADVANCED_FACE ( 'NONE', ( #965 ), #6231, .F. ) ;
#2574=B_SPLINE_CURVE_WITH_KNOTS ( 'NONE', 3,
 ( #660, #3219, #6597, #2129, #1290, #5999 ),
 .UNSPECIFIED., .F., .F.,
 ( 4, 2, 4 ),
 ( -3.640115492409406142E-06, 0.0002066546034006526487, 0.0004169493222937146744 ),
 .UNSPECIFIED. ) ;
#2596=CARTESIAN_POINT ( 'NONE',  ( 0.000000000000000000, 0.000000000000000000, -5.000000000000000888 ) ) ;
#2598=CARTESIAN_POINT ( 'NONE',  ( 4.000000000000000000, -0.8732470631449981147, -3.223155494240760088 ) ) ;
#2614=DIRECTION ( 'NONE',  ( 1.000000000000000000, 0.000000000000000000, 0.000000000000000000 ) ) ;
#2618=CARTESIAN_POINT ( 'NONE',  ( 3.861362476283255685, 2.629030857715988656, -3.671615880910370500 ) ) ;
#2627=CARTESIAN_POINT ( 'NONE',  ( -4.204015924366189871, 1.626724848190922446, -3.610627190413390419 ) ) ;
#2650=CARTESIAN_POINT ( 'NONE',  ( -4.203934362469166963, -1.640673743454851286, -3.598432614606932756 ) ) ;
#2654=CARTESIAN_POINT ( 'NONE',  ( -0.1410422978106123659, 4.700232962125094893, -3.687027686973624707 ) ) ;
#2666=CARTESIAN_POINT ( 'NONE',  ( 2.100000000000000089, 0.000000000000000000, -0.2800830152838844622 ) ) ;
#2681=ORIENTED_EDGE ( 'NONE', *, *, #2965, .F. ) ;
#2685=ORIENTED_EDGE ( 'NONE', *, *, #5051, .T. ) ;
#2687=EDGE_CURVE ( 'NONE', #1419, #5040, #10669, .T. ) ;
#2697=ORIENTED_EDGE ( 'NONE', *, *, #2687, .F. ) ;
#2699=ADVANCED_FACE ( 'NONE', ( #6449 ), #15, .T. ) ;
#2709=CARTESIAN_POINT ( 'NONE',  ( 0.000000000000000000, 0.000000000000000000, 0.000000000000000000 ) ) ;
#2716=ADVANCED_FACE ( 'NONE', ( #1128 ), #9959, .T. ) ;
#2724=DIRECTION ( 'NONE',  ( 1.000000000000000000, 0.000000000000000000, 0.000000000000000000 ) ) ;
#2745=CARTESIAN_POINT ( 'NONE',  ( -4.101948962585906244, 2.368261337751074169, -3.681124513963621503 ) ) ;
#2771=ADVANCED_FACE ( 'NONE', ( #7925 ), #1087, .T. ) ;
#2775=TOROIDAL_SURFACE ( 'NONE', #7372, 5.384454397937118664, 0.5155456020628804703 ) ;
#2781=DIRECTION ( 'NONE',  ( -1.000000000000000000, 0.000000000000000000, 0.000000000000000000 ) ) ;
#2786=CARTESIAN_POINT ( 'NONE',  ( 0.000000000000000000, 0.000000000000000000, -4.974599999999998801 ) ) ;
#2792=ORIENTED_EDGE ( 'NONE', *, *, #4741, .T. ) ;
#2810=ORIENTED_EDGE ( 'NONE', *, *, #2080, .T. ) ;
#2823=ORIENTED_EDGE ( 'NONE', *, *, #6898, .T. ) ;
#2828=CARTESIAN_POINT ( 'NONE',  ( 4.198928548860774157, -0.8158838809860124996, -3.526471437616918170 ) ) ;
#2832=EDGE_CURVE ( 'NONE', #1717, #5040, #4828, .T. ) ;
#2872=EDGE_LOOP ( 'NONE', ( #3605, #3262, #56 ) ) ;
#2873=DIRECTION ( 'NONE',  ( -0.000000000000000000, 0.000000000000000000, -1.000000000000000000 ) ) ;
#2889=EDGE_CURVE ( 'NONE', #3058, #7320, #2162, .T. ) ;
#2892=ORIENTED_EDGE ( 'NONE', *, *, #5196, .F. ) ;
#2909=FACE_OUTER_BOUND ( 'NONE', #1547, .T. ) ;
#2921=CARTESIAN_POINT ( 'NONE',  ( -6.259644161404860030E-16, -4.618802153517027165, -3.433295621305388234 ) ) ;
#2941=AXIS2_PLACEMENT_3D ( 'NONE', #1497, #6942, #6891 ) ;
#2955=AXIS2_PLACEMENT_3D ( 'NONE', #3350, #840, #3405 ) ;
#2965=EDGE_CURVE ( 'NONE', #7506, #4391, #4648, .T. ) ;
#2969=AXIS2_PLACEMENT_3D ( 'NONE', #3135, #9030, #1421 ) ;
#2985=CARTESIAN_POINT ( 'NONE',  ( -4.211140560182196957, 2.431303136016537803, -3.745885042887433514 ) ) ;
#2994=CARTESIAN_POINT ( 'NONE',  ( 0.02448733951239481094, 4.877042772274728044, -3.751161874094022242 ) ) ;
#2999=CARTESIAN_POINT ( 'NONE',  ( -4.175002511812151873, -2.208363329454905877, -3.469254087858246738 ) ) ;
#3013=( NAMED_UNIT ( * ) PLANE_ANGLE_UNIT ( ) SI_UNIT ( $, .RADIAN. ) );
#3029=CARTESIAN_POINT ( 'NONE',  ( 0.000000000000000000, 0.000000000000000000, 0.000000000000000000 ) ) ;
#3034=PRESENTATION_STYLE_ASSIGNMENT (( #3864 ) ) ;
#3040=ADVANCED_FACE ( 'NONE', ( #1943 ), #10674, .T. ) ;
#3044=CARTESIAN_POINT ( 'NONE',  ( -0.6810597143197697489, -4.461075778259609770, -3.598441714920717516 ) ) ;
#3046=ORIENTED_EDGE ( 'NONE', *, *, #9539, .T. ) ;
#3055=ORIENTED_EDGE ( 'NONE', *, *, #8179, .T. ) ;
#3057=CARTESIAN_POINT ( 'NONE',  ( 4.101954839143059139, -2.368264730582948285, -3.681130640444269631 ) ) ;
#3058=VERTEX_POINT ( 'NONE', #2666 ) ;
#3061=VERTEX_POINT ( 'NONE', #9483 ) ;
#3064=CARTESIAN_POINT ( 'NONE',  ( 1.257172072275274388, -3.892973519170983110, -3.433252694550781303 ) ) ;
#3072=ORIENTED_EDGE ( 'NONE', *, *, #1458, .T. ) ;
#3075=CARTESIAN_POINT ( 'NONE',  ( -1.240299975428113101E-15, -4.647091401871173311, -3.572172305156514849 ) ) ;
#3086=CARTESIAN_POINT ( 'NONE',  ( -4.000000000000000000, 0.8730739991738342143, -3.223134629628428893 ) ) ;
#3093=CARTESIAN_POINT ( 'NONE',  ( 2.000000000000008882, 3.464101615137749945, 0.000000000000000000 ) ) ;
#3094=CARTESIAN_POINT ( 'NONE',  ( -3.540020015735593439, -2.810662092924100630, -3.602146406945814672 ) ) ;
#3118=CONICAL_SURFACE ( 'NONE', #6836, 5.560781378645573980, 1.221730476396046816 ) ;
#3135=CARTESIAN_POINT ( 'NONE',  ( 0.000000000000000000, 0.000000000000000000, -25.03750572909317285 ) ) ;
#3138=DIRECTION ( 'NONE',  ( -1.000000000000000000, 0.000000000000000000, 0.000000000000000000 ) ) ;
#3144=VECTOR ( 'NONE', #8753, 1000.000000000000000 ) ;
#3152=CONICAL_SURFACE ( 'NONE', #5994, 2.500000000000000888, 0.9599310885968785900 ) ;
#3167=CARTESIAN_POINT ( 'NONE',  ( 4.141042297810615835, -2.227970268150433863, -3.687027686973623819 ) ) ;
#3171=CARTESIAN_POINT ( 'NONE',  ( 3.999999999999999112, -0.3979232138631231819, -5.929230630780099908E-17 ) ) ;
#3194=CARTESIAN_POINT ( 'NONE',  ( 2.682243648011666703, 3.070208061305304881, -0.04852650426601266831 ) ) ;
#3204=ORIENTED_EDGE ( 'NONE', *, *, #5400, .F. ) ;
#3209=PLANE ( 'NONE',  #8428 ) ;
#3219=CARTESIAN_POINT ( 'NONE',  ( -4.154094228333736538, -2.398367420967545627, -3.721909803043222276 ) ) ;
#3236=AXIS2_PLACEMENT_3D ( 'NONE', #8985, #2264, #5658 ) ;
#3245=CARTESIAN_POINT ( 'NONE',  ( -6.259644161404860030E-16, -4.618802153517027165, -5.000000000000000000 ) ) ;
#3248=ADVANCED_FACE ( 'NONE', ( #3817 ), #8509, .F. ) ;
#3262=ORIENTED_EDGE ( 'NONE', *, *, #7335, .F. ) ;
#3282=DIRECTION ( 'NONE',  ( -0.8191520442889902442, 0.000000000000000000, -0.5735764363510482688 ) ) ;
#3283=VERTEX_POINT ( 'NONE', #10751 ) ;
#3299=ORIENTED_EDGE ( 'NONE', *, *, #9322, .F. ) ;
#3304=CIRCLE ( 'NONE', #6318, 2.100000000000000089 ) ;
#3305=CARTESIAN_POINT ( 'NONE',  ( -4.197312064133472020, -0.8182229787990021874, -3.502518405183886685 ) ) ;
#3311=CARTESIAN_POINT ( 'NONE',  ( 3.349226789952652439, 2.685125164760731487, -0.2236248678334773199 ) ) ;
#3317=EDGE_CURVE ( 'NONE', #10481, #5606, #806, .T. ) ;
#3322=ORIENTED_EDGE ( 'NONE', *, *, #6483, .F. ) ;
#3343=CARTESIAN_POINT ( 'NONE',  ( 0.000000000000000000, 0.000000000000000000, 3.469446951953614189E-15 ) ) ;
#3350=CARTESIAN_POINT ( 'NONE',  ( 0.000000000000000000, 0.000000000000000000, -0.2800830152838844622 ) ) ;
#3355=CARTESIAN_POINT ( 'NONE',  ( -5.384454397937118664, 6.702023979852544604E-16, -5.000000000000000000 ) ) ;
#3357=CARTESIAN_POINT ( 'NONE',  ( 4.197393957002303999, 7.772902908466098641E-14, -3.503767560748929810 ) ) ;
#3361=ADVANCED_FACE ( 'NONE', ( #10200 ), #1205, .F. ) ;
#3396=PLANE ( 'NONE',  #9824 ) ;
#3405=DIRECTION ( 'NONE',  ( 1.000000000000000000, 0.000000000000000000, 0.000000000000000000 ) ) ;
#3437=LINE ( 'NONE', #7603, #5724 ) ;
#3459=VERTEX_POINT ( 'NONE', #3592 ) ;
#3470=CIRCLE ( 'NONE', #5420, 4.000000000000000000 ) ;
#3486=ORIENTED_EDGE ( 'NONE', *, *, #2003, .F. ) ;
#3497=DIRECTION ( 'NONE',  ( 1.000000000000000000, 0.000000000000000000, 0.000000000000000000 ) ) ;
#3503=CARTESIAN_POINT ( 'NONE',  ( 3.510273485745307731, 2.827716139362654424, -3.610536846335885564 ) ) ;
#3508=CARTESIAN_POINT ( 'NONE',  ( -2.344047193898593395, -3.265465875126480455, -1.054683074273691752E-14 ) ) ;
#3515=CONICAL_SURFACE ( 'NONE', #5800, 4.000000000000000000, 0.8911886515913786111 ) ;
#3535=VECTOR ( 'NONE', #9334, 1000.000000000000000 ) ;
#3543=ORIENTED_EDGE ( 'NONE', *, *, #4402, .F. ) ;
#3553=ORIENTED_EDGE ( 'NONE', *, *, #9790, .T. ) ;
#3562=CARTESIAN_POINT ( 'NONE',  ( -4.000000000000000000, -2.309401076758512694, -3.433295621305382461 ) ) ;
#3566=ORIENTED_EDGE ( 'NONE', *, *, #10229, .T. ) ;
#3567=CARTESIAN_POINT ( 'NONE',  ( -2.499999999999999556, 3.061616997868382648E-16, 3.469446951953614189E-15 ) ) ;
#3592=CARTESIAN_POINT ( 'NONE',  ( -2.500000000000000888, 0.000000000000000000, -4.974599999999998801 ) ) ;
#3597=EDGE_CURVE ( 'NONE', #38, #8106, #7449, .T. ) ;
#3599=EDGE_CURVE ( 'NONE', #9170, #8106, #985, .T. ) ;
#3600=DIRECTION ( 'NONE',  ( 0.000000000000000000, 0.000000000000000000, 1.000000000000000000 ) ) ;
#3605=ORIENTED_EDGE ( 'NONE', *, *, #8138, .T. ) ;
#3610=LINE ( 'NONE', #936, #3993 ) ;
#3619=EDGE_LOOP ( 'NONE', ( #7612, #5782, #4671, #8662, #1868 ) ) ;
#3623=CARTESIAN_POINT ( 'NONE',  ( 0.000000000000000000, 0.000000000000000000, -5.000000000000000000 ) ) ;
#3626=CARTESIAN_POINT ( 'NONE',  ( -4.000000000000004441, 2.309401076758496263, -3.504269196027523847 ) ) ;
#3635=CARTESIAN_POINT ( 'NONE',  ( 2.500000000000000444, 0.000000000000000000, -25.03750572909317285 ) ) ;
#3685=CARTESIAN_POINT ( 'NONE',  ( 4.000000000000000000, 2.309401076758497151, -5.000000000000000000 ) ) ;
#3715=EDGE_CURVE ( 'NONE', #6302, #12, #2555, .T. ) ;
#3733=DIRECTION ( 'NONE',  ( 0.000000000000000000, 0.000000000000000000, 1.000000000000000000 ) ) ;
#3751=CARTESIAN_POINT ( 'NONE',  ( -1.393927851585477606, 4.043713361053528743, -3.526374918436835149 ) ) ;
#3754=( NAMED_UNIT ( * ) PLANE_ANGLE_UNIT ( ) SI_UNIT ( $, .RADIAN. ) );
#3763=EDGE_CURVE ( 'NONE', #7320, #6485, #5533, .T. ) ;
#3774=EDGE_CURVE ( 'NONE', #170, #6485, #9690, .T. ) ;
#3775=CARTESIAN_POINT ( 'NONE',  ( -4.000000000000000000, -2.309401076758512694, -3.433295621305382461 ) ) ;
#3789=CYLINDRICAL_SURFACE ( 'NONE', #8123, 2.100000000000000089 ) ;
#3800=CARTESIAN_POINT ( 'NONE',  ( 0.000000000000000000, 0.000000000000000000, 0.000000000000000000 ) ) ;
#3817=FACE_OUTER_BOUND ( 'NONE', #4191, .T. ) ;
#3824=EDGE_CURVE ( 'NONE', #6934, #4635, #3304, .T. ) ;
#3831=VERTEX_POINT ( 'NONE', #3355 ) ;
#3838=( LENGTH_UNIT ( ) NAMED_UNIT ( * ) SI_UNIT ( .MILLI., .METRE. ) );
#3842=CARTESIAN_POINT ( 'NONE',  ( 2.725741868436127202, -3.045094352033990148, -3.220599429844051453 ) ) ;
#3847=CARTESIAN_POINT ( 'NONE',  ( -2.855764796983342624, 2.970025579236414082, -0.09382832055445475272 ) ) ;
#3849=PRODUCT_DEFINITION_SHAPE ( 'NONE', 'NONE',  #6396 ) ;
#3858=FACE_BOUND ( 'NONE', #8467, .T. ) ;
#3864=SURFACE_STYLE_USAGE ( .BOTH. , #7982 ) ;
#3902=ORIENTED_EDGE ( 'NONE', *, *, #6379, .T. ) ;
#3905=EDGE_CURVE ( 'NONE', #3831, #1717, #6848, .T. ) ;
#3907=CARTESIAN_POINT ( 'NONE',  ( 0.000000000000000000, 0.000000000000000000, 0.000000000000000000 ) ) ;
#3918=DIRECTION ( 'NONE',  ( 0.000000000000000000, 0.000000000000000000, -1.000000000000000000 ) ) ;
#3938=CARTESIAN_POINT ( 'NONE',  ( -3.510273485745307287, -2.827716139362669967, -3.610536846335890004 ) ) ;
#3939=ORIENTED_EDGE ( 'NONE', *, *, #2559, .T. ) ;
#3945=CARTESIAN_POINT ( 'NONE',  ( 4.000000000000000000, 2.309401076758497151, -3.433295621305379353 ) ) ;
#3954=DIRECTION ( 'NONE',  ( 1.000000000000000000, 0.000000000000000000, 0.000000000000000000 ) ) ;
#3955=CARTESIAN_POINT ( 'NONE',  ( -1.240299975428134203E-15, -4.736529461165891242, -3.681130640444276292 ) ) ;
#3956=DIRECTION ( 'NONE',  ( 1.000000000000000000, 0.000000000000000000, 0.000000000000000000 ) ) ;
#3965=FACE_OUTER_BOUND ( 'NONE', #8221, .T. ) ;
#3973=ORIENTED_EDGE ( 'NONE', *, *, #6831, .T. ) ;
#3986=ORIENTED_EDGE ( 'NONE', *, *, #9616, .T. ) ;
#3989=FACE_BOUND ( 'NONE', #8269, .T. ) ;
#3992=SHAPE_REPRESENTATION_RELATIONSHIP ( 'NONE' , 'NONE' ,  #6402, #10767 ) ;
#3993=VECTOR ( 'NONE', #6997, 1000.000000000000227 ) ;
#3997=CARTESIAN_POINT ( 'NONE',  ( 3.522875095019493141, -2.820352903225631369, -3.598441714920572299 ) ) ;
#4013=DIRECTION ( 'NONE',  ( -0.000000000000000000, -0.000000000000000000, 1.000000000000000000 ) ) ;
#4016=DIRECTION ( 'NONE',  ( 1.224646799147353207E-16, 1.000000000000000000, 0.000000000000000000 ) ) ;
#4017=EDGE_LOOP ( 'NONE', ( #4439, #5341, #5379 ) ) ;
#4026=CARTESIAN_POINT ( 'NONE',  ( 3.999999999999999112, -1.539600717839012978, -3.300726591567080703 ) ) ;
#4045=VERTEX_POINT ( 'NONE', #6314 ) ;
#4047=ADVANCED_FACE ( 'NONE', ( #9813 ), #6170, .F. ) ;
#4050=ORIENTED_EDGE ( 'NONE', *, *, #7335, .T. ) ;
#4060=CARTESIAN_POINT ( 'NONE',  ( -4.000000000000000000, 2.309401076758498483, -0.4999999999999927280 ) ) ;
#4061=CARTESIAN_POINT ( 'NONE',  ( 4.101954839143060028, 2.368264730582927857, -3.681130640444267854 ) ) ;
#4073=CARTESIAN_POINT ( 'NONE',  ( 1.734723475976807094E-15, 4.618802153517012954, -0.4999999999999995559 ) ) ;
#4081=CYLINDRICAL_SURFACE ( 'NONE', #2969, 2.500000000000000444 ) ;
#4087=CARTESIAN_POINT ( 'NONE',  ( 1.734723475976807094E-15, 4.618802153517012954, -0.4999999999999995559 ) ) ;
#4088=CARTESIAN_POINT ( 'NONE',  ( 4.204115023516791005, -1.660442669500199919, -3.602151381774560068 ) ) ;
#4099=EDGE_CURVE ( 'NONE', #8106, #8932, #1219, .T. ) ;
#4117=ORIENTED_EDGE ( 'NONE', *, *, #5057, .T. ) ;
#4132=PLANE ( 'NONE',  #6148 ) ;
#4151=AXIS2_PLACEMENT_3D ( 'NONE', #7611, #1778, #2724 ) ;
#4157=EDGE_LOOP ( 'NONE', ( #7751, #5730, #9531 ) ) ;
#4176=VECTOR ( 'NONE', #10415, 1000.000000000000000 ) ;
#4191=EDGE_LOOP ( 'NONE', ( #1332, #4334, #10993, #1659 ) ) ;
#4198=CARTESIAN_POINT ( 'NONE',  ( 4.000000000000000888, 1.539600717838996990, -3.300726591567079815 ) ) ;
#4203=CARTESIAN_POINT ( 'NONE',  ( 4.197310751797292738, 0.8178363989516252985, -3.502498386812444409 ) ) ;
#4226=CARTESIAN_POINT ( 'NONE',  ( -4.000000000000000000, 0.7924765000094600165, -0.05906175389889745803 ) ) ;
#4262=DIRECTION ( 'NONE',  ( -1.000000000000000000, 0.000000000000000000, 0.000000000000000000 ) ) ;
#4263=CARTESIAN_POINT ( 'NONE',  ( 2.000000000000008882, 3.464101615137749945, 0.000000000000000000 ) ) ;
#4269=B_SPLINE_CURVE_WITH_KNOTS ( 'NONE', 3,
 ( #9875, #8930, #9820, #9767, #417, #5603, #2265, #579 ),
 .UNSPECIFIED., .F., .F.,
 ( 4, 2, 2, 4 ),
 ( 2.465131517390770070E-07, 0.001183067374689869946, 0.001774477805458935659, 0.002365888236228001588 ),
 .UNSPECIFIED. ) ;
#4277=CARTESIAN_POINT ( 'NONE',  ( 0.000000000000000000, 0.000000000000000000, -5.000000000000000000 ) ) ;
#4284=CARTESIAN_POINT ( 'NONE',  ( -3.679171394226034675, -2.494631558665844739, -0.3503314178412558211 ) ) ;
#4285=DIRECTION ( 'NONE',  ( -1.000000000000000000, 0.000000000000000000, 0.000000000000000000 ) ) ;
#4287=AXIS2_PLACEMENT_3D ( 'NONE', #349, #7187, #6241 ) ;
#4296=DIRECTION ( 'NONE',  ( 0.000000000000000000, 0.000000000000000000, 1.000000000000000000 ) ) ;
#4306=ORIENTED_EDGE ( 'NONE', *, *, #2031, .F. ) ;
#4313=CARTESIAN_POINT ( 'NONE',  ( 4.235886605889389145, 2.417314728048528760, -3.751161874094018245 ) ) ;
#4318=CARTESIAN_POINT ( 'NONE',  ( 2.345747346278113987, -3.264484291692503870, -0.01223254789874484924 ) ) ;
#4334=ORIENTED_EDGE ( 'NONE', *, *, #6882, .F. ) ;
#4375=CARTESIAN_POINT ( 'NONE',  ( 2.290893957444128645E-15, 4.647089433458768681, -3.572167766733382877 ) ) ;
#4376=CARTESIAN_POINT ( 'NONE',  ( 2.687328764639642653, -3.067272167851299969, -0.05923475698271395140 ) ) ;
#4385=CARTESIAN_POINT ( 'NONE',  ( 4.000000000000000000, -2.309401076758514915, -5.000000000000000000 ) ) ;
#4391=VERTEX_POINT ( 'NONE', #1808 ) ;
#4402=EDGE_CURVE ( 'NONE', #3459, #7216, #8814, .T. ) ;
#4406=B_SPLINE_CURVE_WITH_KNOTS ( 'NONE', 3,
 ( #4087, #5751, #9815, #688, #9193, #2202, #8982, #3093 ),
 .UNSPECIFIED., .F., .F.,
 ( 4, 2, 2, 4 ),
 ( 2.465131517075058656E-07, 0.001183067374689851080, 0.001774477805458923299, 0.002365888236227995517 ),
 .UNSPECIFIED. ) ;
#4409=DIRECTION ( 'NONE',  ( 1.000000000000000000, 0.000000000000000000, 0.000000000000000000 ) ) ;
#4411=EDGE_LOOP ( 'NONE', ( #5910, #8111, #8513, #3486 ) ) ;
#4415=ORIENTED_EDGE ( 'NONE', *, *, #441, .T. ) ;
#4428=VECTOR ( 'NONE', #2426, 1000.000000000000000 ) ;
#4434=CARTESIAN_POINT ( 'NONE',  ( 1.287237434362044075, 3.875615274277557809, -3.430618716626812059 ) ) ;
#4438=CARTESIAN_POINT ( 'NONE',  ( 3.355112389629172576, -2.681727112203168950, -0.2256878752776777242 ) ) ;
#4439=ORIENTED_EDGE ( 'NONE', *, *, #1924, .T. ) ;
#4440=DIRECTION ( 'NONE',  ( 1.000000000000000000, 0.000000000000000000, 0.000000000000000000 ) ) ;
#4450=ORIENTED_EDGE ( 'NONE', *, *, #3599, .F. ) ;
#4470=B_SPLINE_CURVE_WITH_KNOTS ( 'NONE', 3,
 ( #8530, #9358, #2523, #6858, #5091 ),
 .UNSPECIFIED., .F., .F.,
 ( 4, 1, 4 ),
 ( 0.000000000000000000, 0.002309401076758505790, 0.004618802153517011580 ),
 .UNSPECIFIED. ) ;
#4475=CARTESIAN_POINT ( 'NONE',  ( -4.000000000000000000, 2.309401076758498483, -0.4999999999999927280 ) ) ;
#4535=ADVANCED_FACE ( 'NONE', ( #3965 ), #4081, .F. ) ;
#4550=CIRCLE ( 'NONE', #5609, 5.384454397937118664 ) ;
#4580=CARTESIAN_POINT ( 'NONE',  ( -2.345747346278108214, 3.264484291692489215, -0.01223254789873409049 ) ) ;
#4581=DIRECTION ( 'NONE',  ( 0.000000000000000000, 0.000000000000000000, 1.000000000000000000 ) ) ;
#4596=CARTESIAN_POINT ( 'NONE',  ( -0.6937372685066653943, 4.453844082567723461, -3.610536846335889116 ) ) ;
#4600=ADVANCED_FACE ( 'NONE', ( #9809 ), #5246, .F. ) ;
#4611=ORIENTED_EDGE ( 'NONE', *, *, #9114, .T. ) ;
#4635=VERTEX_POINT ( 'NONE', #5745 ) ;
#4648=B_SPLINE_CURVE_WITH_KNOTS ( 'NONE', 3,
 ( #7401, #6562, #8288, #8344, #676, #4073 ),
 .UNSPECIFIED., .F., .F.,
 ( 4, 2, 4 ),
 ( 0.002365888236227977302, 0.003551327329835078910, 0.004736766423442180518 ),
 .UNSPECIFIED. ) ;
#4656=ADVANCED_FACE ( 'NONE', ( #10855 ), #8800, .F. ) ;
#4671=ORIENTED_EDGE ( 'NONE', *, *, #6135, .T. ) ;
#4678=B_SPLINE_CURVE_WITH_KNOTS ( 'NONE', 3,
 ( #5285, #3508, #8503, #166, #4284, #7674 ),
 .UNSPECIFIED., .F., .F.,
 ( 4, 2, 4 ),
 ( 0.002365888236228001588, 0.003551327329835089319, 0.004736766423442177049 ),
 .UNSPECIFIED. ) ;
#4679=SURFACE_STYLE_USAGE ( .BOTH. , #2125 ) ;
#4688=DIRECTION ( 'NONE',  ( 0.000000000000000000, 0.000000000000000000, 1.000000000000000000 ) ) ;
#4689=EDGE_LOOP ( 'NONE', ( #8781, #2810, #3046, #8292, #729 ) ) ;
#4690=ORIENTED_EDGE ( 'NONE', *, *, #441, .F. ) ;
#4693=AXIS2_PLACEMENT_3D ( 'NONE', #10213, #10107, #3497 ) ;
#4706=CARTESIAN_POINT ( 'NONE',  ( 0.000000000000000000, 0.000000000000000000, -0.3080913168122742518 ) ) ;
#4714=CARTESIAN_POINT ( 'NONE',  ( -2.742827927723112236, -3.035229711105190464, -3.433252694550595230 ) ) ;
#4715=CONICAL_SURFACE ( 'NONE', #5069, 2.500000000000000888, 0.9599310885968785900 ) ;
#4721=ADVANCED_FACE ( 'NONE', ( #907 ), #4132, .T. ) ;
#4736=SURFACE_STYLE_FILL_AREA ( #5564 ) ;
#4741=EDGE_CURVE ( 'NONE', #8576, #990, #4470, .T. ) ;
#4742=ADVANCED_FACE ( 'NONE', ( #5199 ), #8612, .T. ) ;
#4743=CARTESIAN_POINT ( 'NONE',  ( 4.211140560182196957, 2.431303136016536470, -3.745885042887433514 ) ) ;
#4755=DIRECTION ( 'NONE',  ( -0.000000000000000000, -0.000000000000000000, 1.000000000000000000 ) ) ;
#4762=CIRCLE ( 'NONE', #8841, 2.499999999999999556 ) ;
#4765=CARTESIAN_POINT ( 'NONE',  ( -4.000000000000000000, 1.677772373332757194, -3.535253723897187506 ) ) ;
#4773=VERTEX_POINT ( 'NONE', #9187 ) ;
#4779=CARTESIAN_POINT ( 'NONE',  ( 2.000000000000000444, 3.464101615137754830, -3.142992957459231018 ) ) ;
#4786=ORIENTED_EDGE ( 'NONE', *, *, #2003, .T. ) ;
#4788=( LENGTH_UNIT ( ) NAMED_UNIT ( * ) SI_UNIT ( .MILLI., .METRE. ) );
#4802=B_SPLINE_CURVE_WITH_KNOTS ( 'NONE', 3,
 ( #8481, #864, #8539, #7533 ),
 .UNSPECIFIED., .F., .F.,
 ( 4, 4 ),
 ( 0.000000000000000000, 0.002452478801916376308 ),
 .UNSPECIFIED. ) ;
#4811=VERTEX_POINT ( 'NONE', #1125 ) ;
#4817=CARTESIAN_POINT ( 'NONE',  ( -2.725741868435985094, 3.045094352034055429, -3.220599429844047012 ) ) ;
#4828=CIRCLE ( 'NONE', #8900, 5.560781378645573980 ) ;
#4842=CARTESIAN_POINT ( 'NONE',  ( -0.1750025118121544265, -4.719839900820635314, -3.469254087858253399 ) ) ;
#4870=AXIS2_PLACEMENT_3D ( 'NONE', #8663, #2781, #10442 ) ;
#4872=CARTESIAN_POINT ( 'NONE',  ( 4.000000000000000000, 2.512223110932545023, -3.469391141908803711 ) ) ;
#4900=CARTESIAN_POINT ( 'NONE',  ( 2.807080416178989513, -3.225969019225150003, -3.502507215260505014 ) ) ;
#4902=CIRCLE ( 'NONE', #2955, 2.100000000000000089 ) ;
#4907=PRODUCT_DEFINITION_CONTEXT ( 'detailed design', #10976, 'design' ) ;
#4908=EDGE_CURVE ( 'NONE', #8322, #7216, #237, .T. ) ;
#4911=EDGE_LOOP ( 'NONE', ( #2521, #1441, #3072, #9986, #7950, #8373, #5951 ) ) ;
#4918=DIRECTION ( 'NONE',  ( -0.000000000000000000, -0.000000000000000000, 1.000000000000000000 ) ) ;
#4924=CARTESIAN_POINT ( 'NONE',  ( -4.000000000000000000, 2.511478553582031203, -3.469254451724764543 ) ) ;
#4933=CARTESIAN_POINT ( 'NONE',  ( -4.197393957002303999, -7.773935952363655451E-14, -3.503767560748929810 ) ) ;
#4956=CIRCLE ( 'NONE', #6368, 4.000000000000000000 ) ;
#4981=CARTESIAN_POINT ( 'NONE',  ( 4.211140560182196957, 2.431303136016536470, -3.745885042887433514 ) ) ;
#4998=ORIENTED_EDGE ( 'NONE', *, *, #9929, .T. ) ;
#5003=FACE_OUTER_BOUND ( 'NONE', #5087, .T. ) ;
#5011=CARTESIAN_POINT ( 'NONE',  ( 4.000000000000000000, 0.1981133338132474442, 2.382280164152719704E-17 ) ) ;
#5014=ORIENTED_EDGE ( 'NONE', *, *, #6831, .F. ) ;
#5026=DIRECTION ( 'NONE',  ( 0.000000000000000000, 0.000000000000000000, -1.000000000000000000 ) ) ;
#5031=ORIENTED_EDGE ( 'NONE', *, *, #3824, .T. ) ;
#5033=CARTESIAN_POINT ( 'NONE',  ( -4.000000000000000000, -1.680117682357936904, -3.316611593218794951 ) ) ;
#5040=VERTEX_POINT ( 'NONE', #9200 ) ;
#5044=CARTESIAN_POINT ( 'NONE',  ( -4.000000000000000000, -2.309401076758512694, -5.000000000000000000 ) ) ;
#5051=EDGE_CURVE ( 'NONE', #4811, #8576, #10945, .T. ) ;
#5057=EDGE_CURVE ( 'NONE', #990, #6444, #7652, .T. ) ;
#5069=AXIS2_PLACEMENT_3D ( 'NONE', #2786, #1784, #6160 ) ;
#5070=DIRECTION ( 'NONE',  ( 0.000000000000000000, 0.000000000000000000, 1.000000000000000000 ) ) ;
#5087=EDGE_LOOP ( 'NONE', ( #5450, #2685, #5741, #8601, #1673 ) ) ;
#5091=CARTESIAN_POINT ( 'NONE',  ( -4.000000000000000000, -2.309401076758512694, -3.433295621305382461 ) ) ;
#5098=CARTESIAN_POINT ( 'NONE',  ( 2.344047193898588954, 3.265465875126468021, -5.031375706690542042E-16 ) ) ;
#5103=CARTESIAN_POINT ( 'NONE',  ( -1.999999999999999556, 3.464101615137754830, -3.142992957459232795 ) ) ;
#5125=DIRECTION ( 'NONE',  ( 0.000000000000000000, 0.000000000000000000, -1.000000000000000000 ) ) ;
#5152=CARTESIAN_POINT ( 'NONE',  ( 5.384454397937118664, 0.000000000000000000, -4.484454397937119197 ) ) ;
#5157=ORIENTED_EDGE ( 'NONE', *, *, #6469, .T. ) ;
#5163=DIRECTION ( 'NONE',  ( 0.000000000000000000, -0.000000000000000000, 1.000000000000000000 ) ) ;
#5196=EDGE_CURVE ( 'NONE', #5966, #10907, #6304, .T. ) ;
#5199=FACE_OUTER_BOUND ( 'NONE', #7579, .T. ) ;
#5209=CARTESIAN_POINT ( 'NONE',  ( 2.000000000000005329, -3.464101615137751722, 0.000000000000000000 ) ) ;
#5224=ORIENTED_EDGE ( 'NONE', *, *, #2396, .F. ) ;
#5226=CARTESIAN_POINT ( 'NONE',  ( 1.411581201560190495E-15, 4.862606272033091592, -3.745885042887436622 ) ) ;
#5237=AXIS2_PLACEMENT_3D ( 'NONE', #6984, #7879, #9703 ) ;
#5246=CONICAL_SURFACE ( 'NONE', #10913, 2.059999999999998721, 0.9599310885968738161 ) ;
#5258=CARTESIAN_POINT ( 'NONE',  ( 2.836893136758676270, 3.208949435745843903, -3.505054077164911241 ) ) ;
#5260=CARTESIAN_POINT ( 'NONE',  ( 1.411581201560190495E-15, 4.862606272033091592, -3.745885042887436622 ) ) ;
#5280=ORIENTED_EDGE ( 'NONE', *, *, #1583, .F. ) ;
#5285=CARTESIAN_POINT ( 'NONE',  ( -2.000000000000007550, -3.464101615137749945, 0.000000000000000000 ) ) ;
#5305=ORIENTED_EDGE ( 'NONE', *, *, #5051, .F. ) ;
#5307=STYLED_ITEM ( 'NONE', ( #3034 ), #5578 ) ;
#5313=CARTESIAN_POINT ( 'NONE',  ( -0.1756481739660520902, 4.720212674038980261, -3.469390959564065291 ) ) ;
#5341=ORIENTED_EDGE ( 'NONE', *, *, #9616, .F. ) ;
#5363=CARTESIAN_POINT ( 'NONE',  ( 2.742827927723449299, 3.035229711104609596, -3.433252694550591233 ) ) ;
#5373=CYLINDRICAL_SURFACE ( 'NONE', #5237, 2.500000000000000444 ) ;
#5379=ORIENTED_EDGE ( 'NONE', *, *, #892, .F. ) ;
#5400=EDGE_CURVE ( 'NONE', #6302, #8576, #471, .T. ) ;
#5401=CIRCLE ( 'NONE', #4693, 2.500000000000000888 ) ;
#5420=AXIS2_PLACEMENT_3D ( 'NONE', #1025, #10981, #4262 ) ;
#5434=CARTESIAN_POINT ( 'NONE',  ( -3.455068668934486276, 2.624017327439035707, -3.316620875263955437 ) ) ;
#5446=CARTESIAN_POINT ( 'NONE',  ( 3.333333333333332593, 2.694301256218250007, -3.300726591567078483 ) ) ;
#5450=ORIENTED_EDGE ( 'NONE', *, *, #6135, .F. ) ;
#5465=CARTESIAN_POINT ( 'NONE',  ( 1.567478505476134606E-15, 4.618802153517012066, -5.000000000000000000 ) ) ;
#5482=CARTESIAN_POINT ( 'NONE',  ( -3.511755186886750479, 2.826662030176366081, -3.597382984111578086 ) ) ;
#5484=CARTESIAN_POINT ( 'NONE',  ( 0.000000000000000000, 0.000000000000000000, 0.000000000000000000 ) ) ;
#5494=CARTESIAN_POINT ( 'NONE',  ( -4.175648173966055587, 2.207990556236529844, -3.469390959564062626 ) ) ;
#5500=LINE ( 'NONE', #10444, #7528 ) ;
#5512=FILL_AREA_STYLE_COLOUR ( '', #1367 ) ;
#5519=CARTESIAN_POINT ( 'NONE',  ( 5.560781378645573980, 6.809993116116507654E-16, -4.000000000000000000 ) ) ;
#5528=CARTESIAN_POINT ( 'NONE',  ( 4.000000000000000000, -2.309401076758514915, -3.433295621305383349 ) ) ;
#5529=DIRECTION ( 'NONE',  ( -1.000000000000000000, 0.000000000000000000, 0.000000000000000000 ) ) ;
#5533=LINE ( 'NONE', #1466, #104 ) ;
#5535=( LENGTH_UNIT ( ) NAMED_UNIT ( * ) SI_UNIT ( .MILLI., .METRE. ) );
#5546=CARTESIAN_POINT ( 'NONE',  ( -3.453038570459499024, -2.625189405340453419, -3.535263753545272891 ) ) ;
#5564=FILL_AREA_STYLE ('',( #5512 ) ) ;
#5568=ADVANCED_FACE ( 'NONE', ( #6927 ), #10315, .F. ) ;
#5570=CARTESIAN_POINT ( 'NONE',  ( -0.02448733951239248641, -4.877042772274742255, -3.751161874094027571 ) ) ;
#5578=MANIFOLD_SOLID_BREP ( 'EndChamfer', #7010 ) ;
#5580=DIRECTION ( 'NONE',  ( 1.000000000000000000, 0.000000000000000000, 0.000000000000000000 ) ) ;
#5584=CARTESIAN_POINT ( 'NONE',  ( -2.805705207896067144, 3.226868319750155312, -3.503898532754364581 ) ) ;
#5594=CARTESIAN_POINT ( 'NONE',  ( -0.5469614295416921346, 4.303013824936271270, -3.535263753543735454 ) ) ;
#5596=CARTESIAN_POINT ( 'NONE',  ( 1.393927851585479161, -4.043713361053543842, -3.526374918436840922 ) ) ;
#5597=CARTESIAN_POINT ( 'NONE',  ( -1.287237434361707233, -3.875615274277397937, -3.430618716626816500 ) ) ;
#5603=CARTESIAN_POINT ( 'NONE',  ( -1.654252653721913102, -3.663718938583024443, -0.01223254789874440342 ) ) ;
#5606=VERTEX_POINT ( 'NONE', #10646 ) ;
#5608=CARTESIAN_POINT ( 'NONE',  ( -4.000000000000000000, 2.309401076758498483, -3.433295621305379353 ) ) ;
#5609=AXIS2_PLACEMENT_3D ( 'NONE', #5634, #10637, #5580 ) ;
#5615=ORIENTED_EDGE ( 'NONE', *, *, #693, .F. ) ;
#5619=( NAMED_UNIT ( * ) SI_UNIT ( $, .STERADIAN. ) SOLID_ANGLE_UNIT ( ) );
#5631=ORIENTED_EDGE ( 'NONE', *, *, #2477, .T. ) ;
#5634=CARTESIAN_POINT ( 'NONE',  ( 0.000000000000000000, 0.000000000000000000, -5.000000000000000000 ) ) ;
#5637=CARTESIAN_POINT ( 'NONE',  ( 0.6666666666666658525, -4.233901974057276085, -3.300726591567086476 ) ) ;
#5643=FACE_OUTER_BOUND ( 'NONE', #9655, .T. ) ;
#5648=CARTESIAN_POINT ( 'NONE',  ( -4.197477534772231955, 0.8522413273724368521, -3.505042416683225692 ) ) ;
#5651=CARTESIAN_POINT ( 'NONE',  ( -1.243802165048909503, 3.900692638707381921, -3.223146290109805800 ) ) ;
#5653=CARTESIAN_POINT ( 'NONE',  ( 4.211140560182196957, -2.431303136016555122, -3.745885042887436622 ) ) ;
#5655=CARTESIAN_POINT ( 'NONE',  ( 0.1756481739660539498, -4.720212674038995360, -3.469390959564070620 ) ) ;
#5658=DIRECTION ( 'NONE',  ( -1.000000000000000000, 0.000000000000000000, 0.000000000000000000 ) ) ;
#5666=EDGE_CURVE ( 'NONE', #7952, #3459, #304, .T. ) ;
#5675=CARTESIAN_POINT ( 'NONE',  ( 2.712762565639649015, -3.052587955997662306, -3.430618716626630871 ) ) ;
#5685=EDGE_CURVE ( 'NONE', #7847, #7506, #1735, .T. ) ;
#5693=DIRECTION ( 'NONE',  ( 0.000000000000000000, 0.000000000000000000, -1.000000000000000000 ) ) ;
#5698=CARTESIAN_POINT ( 'NONE',  ( 0.000000000000000000, 0.000000000000000000, -4.000000000000000000 ) ) ;
#5700=CARTESIAN_POINT ( 'NONE',  ( 4.000000000000000000, -1.084202172485504434E-14, -3.142992957459231906 ) ) ;
#5717=CARTESIAN_POINT ( 'NONE',  ( 4.154306624731035846, -2.398490048085128556, -3.721999068284417955 ) ) ;
#5724=VECTOR ( 'NONE', #1651, 1000.000000000000000 ) ;
#5730=ORIENTED_EDGE ( 'NONE', *, *, #5685, .T. ) ;
#5740=DIRECTION ( 'NONE',  ( -1.000000000000000000, 1.224646799147352714E-16, 0.000000000000000000 ) ) ;
#5741=ORIENTED_EDGE ( 'NONE', *, *, #1068, .T. ) ;
#5742=PLANE ( 'NONE',  #2262 ) ;
#5743=ORIENTED_EDGE ( 'NONE', *, *, #6898, .F. ) ;
#5745=CARTESIAN_POINT ( 'NONE',  ( 2.100000000000000089, 0.000000000000000000, -4.694516984716113228 ) ) ;
#5751=CARTESIAN_POINT ( 'NONE',  ( 0.3198814748697593746, 4.434118497892183264, -0.3507732604232499107 ) ) ;
#5768=CARTESIAN_POINT ( 'NONE',  ( -2.804994570502171047, -3.229033611042465335, -3.526374918436838701 ) ) ;
#5775=CARTESIAN_POINT ( 'NONE',  ( -4.000000000000000000, 0.000000000000000000, 0.000000000000000000 ) ) ;
#5782=ORIENTED_EDGE ( 'NONE', *, *, #9399, .T. ) ;
#5784=ORIENTED_EDGE ( 'NONE', *, *, #10229, .F. ) ;
#5789=CARTESIAN_POINT ( 'NONE',  ( 0.000000000000000000, 0.000000000000000000, -4.000000000000000000 ) ) ;
#5791=CARTESIAN_POINT ( 'NONE',  ( 0.000000000000000000, 0.000000000000000000, -4.694516984716113228 ) ) ;
#5794=ADVANCED_FACE ( 'NONE', ( #10798 ), #5742, .T. ) ;
#5795=ORIENTED_EDGE ( 'NONE', *, *, #3715, .T. ) ;
#5800=AXIS2_PLACEMENT_3D ( 'NONE', #9180, #5693, #2249 ) ;
#5803=DIRECTION ( 'NONE',  ( 0.000000000000000000, 0.000000000000000000, -1.000000000000000000 ) ) ;
#5807=CARTESIAN_POINT ( 'NONE',  ( 4.203935335434060505, 1.640780671294165272, -3.598452447879202598 ) ) ;
#5824=FILL_AREA_STYLE_COLOUR ( '', #10092 ) ;
#5827=ORIENTED_EDGE ( 'NONE', *, *, #7998, .T. ) ;
#5830=DIRECTION ( 'NONE',  ( -0.5000000000000016653, 0.8660254037844378194, 0.000000000000000000 ) ) ;
#5842=ORIENTED_EDGE ( 'NONE', *, *, #3905, .F. ) ;
#5849=ADVANCED_FACE ( 'NONE', ( #5643 ), #3515, .T. ) ;
#5852=CARTESIAN_POINT ( 'NONE',  ( 4.000000000000000000, -2.309401076758516691, -0.4999999999999995559 ) ) ;
#5856=CARTESIAN_POINT ( 'NONE',  ( 0.3208286057739604957, -4.433571671609698228, -0.3503314178412692548 ) ) ;
#5891=B_SPLINE_CURVE_WITH_KNOTS ( 'NONE', 3,
 ( #5775, #10113, #7441, #4226, #7615, #7496, #1299, #4060 ),
 .UNSPECIFIED., .F., .F.,
 ( 4, 2, 2, 4 ),
 ( 0.005725059856848641743, 0.006314084072593626612, 0.006903108288338611481, 0.008081156719828581220 ),
 .UNSPECIFIED. ) ;
#5893=ORIENTED_EDGE ( 'NONE', *, *, #10640, .F. ) ;
#5910=ORIENTED_EDGE ( 'NONE', *, *, #3824, .F. ) ;
#5912=CARTESIAN_POINT ( 'NONE',  ( -4.000000000000000000, -0.8382240730041925492, -3.220610619767135141 ) ) ;
#5924=CARTESIAN_POINT ( 'NONE',  ( -4.000000000000000000, -2.309401076758515803, -0.4999999999999995559 ) ) ;
#5945=PLANE ( 'NONE',  #10792 ) ;
#5951=ORIENTED_EDGE ( 'NONE', *, *, #2832, .T. ) ;
#5966=VERTEX_POINT ( 'NONE', #3357 ) ;
#5973=LINE ( 'NONE', #7757, #1444 ) ;
#5977=CARTESIAN_POINT ( 'NONE',  ( 4.000000000000000000, 1.680228229147133767, -3.316631783032546021 ) ) ;
#5993=ORIENTED_EDGE ( 'NONE', *, *, #1888, .F. ) ;
#5994=AXIS2_PLACEMENT_3D ( 'NONE', #999, #10176, #55 ) ;
#5995=DIRECTION ( 'NONE',  ( -0.000000000000000000, -0.000000000000000000, 1.000000000000000000 ) ) ;
#5999=CARTESIAN_POINT ( 'NONE',  ( -4.000000000000000000, -2.309401076758512694, -3.433295621305382461 ) ) ;
#6029=CARTESIAN_POINT ( 'NONE',  ( 3.472371940585993855, 2.614027278893175321, -3.320322319201766792 ) ) ;
#6059=ORIENTED_EDGE ( 'NONE', *, *, #693, .T. ) ;
#6100=CARTESIAN_POINT ( 'NONE',  ( 2.804994570502171047, 3.229033611042449792, -3.526374918436834704 ) ) ;
#6106=FACE_OUTER_BOUND ( 'NONE', #4017, .T. ) ;
#6135=EDGE_CURVE ( 'NONE', #4811, #4391, #6284, .T. ) ;
#6137=CARTESIAN_POINT ( 'NONE',  ( -3.974344831685191280E-13, 4.796734841935104576, -3.721909803043223608 ) ) ;
#6147=EDGE_CURVE ( 'NONE', #4773, #5606, #1177, .T. ) ;
#6148=AXIS2_PLACEMENT_3D ( 'NONE', #3245, #10192, #10138 ) ;
#6152=( GEOMETRIC_REPRESENTATION_CONTEXT ( 3 ) GLOBAL_UNCERTAINTY_ASSIGNED_CONTEXT ( ( #1875 ) ) GLOBAL_UNIT_ASSIGNED_CONTEXT ( ( #4788, #6547, #7274 ) ) REPRESENTATION_CONTEXT ( 'NONE', 'WORKASPACE' ) );
#6158=ORIENTED_EDGE ( 'NONE', *, *, #7702, .F. ) ;
#6160=DIRECTION ( 'NONE',  ( -1.000000000000000000, 0.000000000000000000, 0.000000000000000000 ) ) ;
#6170=( BOUNDED_SURFACE ( )  B_SPLINE_SURFACE ( 3, 2, ( 
 ( #9705, #10597, #2994 ),
 ( #8195, #5594, #8980 ),
 ( #5651, #1370, #1424 ),
 ( #4817, #6253, #2040 ),
 ( #5434, #10541, #2101 ),
 ( #5494, #8878, #412 ) ),
 .UNSPECIFIED., .F., .F., .T. ) 
 B_SPLINE_SURFACE_WITH_KNOTS ( ( 4, 2, 4 ),
 ( 3, 3 ),
 ( 0.02032853247518125531, 0.02278863295364820865, 0.02524873343211516200 ),
 ( 0.000000000000000000, 1.000000000000000000 ),
 .UNSPECIFIED. ) 
 GEOMETRIC_REPRESENTATION_ITEM ( )  RATIONAL_B_SPLINE_SURFACE ( (
 ( 1.000000000000000000, 0.8047781615896836271, 1.000000000000000000),
 ( 1.000000000000000000, 0.8123767586289967202, 1.000000000000000000),
 ( 1.000000000000000000, 0.8190662415563443322, 1.000000000000000000),
 ( 1.000000000000000000, 0.8192361015669982205, 1.000000000000000000),
 ( 1.000000000000000000, 0.8126135807103181952, 1.000000000000000000),
 ( 1.000000000000000000, 0.8047712338318587788, 1.000000000000000000) ) ) 
 REPRESENTATION_ITEM ( '' )  SURFACE ( )  );
#6182=AXIS2_PLACEMENT_3D ( 'NONE', #2596, #8868, #10531 ) ;
#6199=UNCERTAINTY_MEASURE_WITH_UNIT (LENGTH_MEASURE( 1.000000000000000082E-05 ), #3838, 'distance_accuracy_value', 'NONE');
#6207=ORIENTED_EDGE ( 'NONE', *, *, #2832, .F. ) ;
#6216=CARTESIAN_POINT ( 'NONE',  ( 0.6666666666666689611, 4.233901974057261874, -3.300726591567082480 ) ) ;
#6231=( BOUNDED_SURFACE ( )  B_SPLINE_SURFACE ( 3, 2, ( 
 ( #6920, #9363, #4313 ),
 ( #6029, #76, #1926 ),
 ( #10309, #5363, #5258 ),
 ( #7868, #4434, #8746 ),
 ( #9469, #7644, #138 ),
 ( #5313, #2654, #9578 ) ),
 .UNSPECIFIED., .F., .F., .F. ) 
 B_SPLINE_SURFACE_WITH_KNOTS ( ( 4, 2, 4 ),
 ( 3, 3 ),
 ( 0.02032853247518126225, 0.02278863295364821212, 0.02524873343211516200 ),
 ( 0.000000000000000000, 1.000000000000000000 ),
 .UNSPECIFIED. ) 
 GEOMETRIC_REPRESENTATION_ITEM ( )  RATIONAL_B_SPLINE_SURFACE ( (
 ( 1.000000000000000000, 0.8047781615896835161, 1.000000000000000000),
 ( 1.000000000000000000, 0.8123767586291043008, 1.000000000000000000),
 ( 1.000000000000000000, 0.8190662415562011134, 1.000000000000000000),
 ( 1.000000000000000000, 0.8192361015671398849, 1.000000000000000000),
 ( 1.000000000000000000, 0.8126135807102121689, 1.000000000000000000),
 ( 1.000000000000000000, 0.8047712338318585568, 1.000000000000000000) ) ) 
 REPRESENTATION_ITEM ( '' )  SURFACE ( )  );
#6241=DIRECTION ( 'NONE',  ( -1.000000000000000000, 0.000000000000000000, 0.000000000000000000 ) ) ;
#6245=EDGE_LOOP ( 'NONE', ( #5784, #6158 ) ) ;
#6246=SURFACE_STYLE_FILL_AREA ( #2146 ) ;
#6253=CARTESIAN_POINT ( 'NONE',  ( -2.712762565639006418, 3.052587955997511759, -3.430618716626627318 ) ) ;
#6274=ORIENTED_EDGE ( 'NONE', *, *, #1924, .F. ) ;
#6284=LINE ( 'NONE', #5465, #2430 ) ;
#6302=VERTEX_POINT ( 'NONE', #1561 ) ;
#6304=B_SPLINE_CURVE_WITH_KNOTS ( 'NONE', 3,
 ( #309, #9477, #2828, #7141, #2035, #1873 ),
 .UNSPECIFIED., .F., .F.,
 ( 4, 2, 4 ),
 ( 0.002452478801916361129, 0.003676905084148001344, 0.004901331366379641126 ),
 .UNSPECIFIED. ) ;
#6314=CARTESIAN_POINT ( 'NONE',  ( -4.211140560182196957, -2.431303136016552013, -3.745885042887436178 ) ) ;
#6318=AXIS2_PLACEMENT_3D ( 'NONE', #5791, #10077, #7514 ) ;
#6319=ORIENTED_EDGE ( 'NONE', *, *, #192, .T. ) ;
#6339=DIRECTION ( 'NONE',  ( 1.000000000000000000, 0.000000000000000000, 0.000000000000000000 ) ) ;
#6355=CARTESIAN_POINT ( 'NONE',  ( 3.333333333333335702, -2.694301256218268215, -3.300726591567084256 ) ) ;
#6368=AXIS2_PLACEMENT_3D ( 'NONE', #6660, #8446, #6451 ) ;
#6376=CARTESIAN_POINT ( 'NONE',  ( -4.235886605889389145, -2.417314728048544303, -3.751161874094020909 ) ) ;
#6377=ORIENTED_EDGE ( 'NONE', *, *, #6483, .T. ) ;
#6378=CARTESIAN_POINT ( 'NONE',  ( -2.000000000000007550, -3.464101615137749945, 0.000000000000000000 ) ) ;
#6379=EDGE_CURVE ( 'NONE', #6934, #3459, #10002, .T. ) ;
#6388=DIRECTION ( 'NONE',  ( 0.000000000000000000, 0.000000000000000000, -1.000000000000000000 ) ) ;
#6393=CARTESIAN_POINT ( 'NONE',  ( 3.436319922986518449, -2.634841920959471562, -3.531542292954761741 ) ) ;
#6396=PRODUCT_DEFINITION ( 'UNKNOWN', '', #8462, #4907 ) ;
#6402=SHAPE_REPRESENTATION ( 'hex flange nut gradea_iso_ISO - 4161 - M5 - N', ( #308 ), #6687 ) ;
#6403=DIRECTION ( 'NONE',  ( 0.000000000000000000, 0.000000000000000000, -1.000000000000000000 ) ) ;
#6404=CARTESIAN_POINT ( 'NONE',  ( 4.000000000000000000, 0.7924765000094659007, -0.05906175389889852662 ) ) ;
#6412=DIRECTION ( 'NONE',  ( 1.000000000000000000, 0.000000000000000000, 0.000000000000000000 ) ) ;
#6418=CARTESIAN_POINT ( 'NONE',  ( 0.02511973781850649831, -4.877415612947427981, -3.751298745799844792 ) ) ;
#6419=B_SPLINE_CURVE_WITH_KNOTS ( 'NONE', 3,
 ( #5924, #9311, #9704, #10596, #2039, #9645 ),
 .UNSPECIFIED., .F., .F.,
 ( 4, 2, 4 ),
 ( 0.003358874760055550156, 0.004541967308452096383, 0.005725059856848641743 ),
 .UNSPECIFIED. ) ;
#6433=DIRECTION ( 'NONE',  ( -1.000000000000000000, 0.000000000000000000, 0.000000000000000000 ) ) ;
#6437=ORIENTED_EDGE ( 'NONE', *, *, #9192, .F. ) ;
#6444=VERTEX_POINT ( 'NONE', #6903 ) ;
#6448=CARTESIAN_POINT ( 'NONE',  ( -3.264650091097280831E-13, -4.796980096169642493, -3.721999068284424617 ) ) ;
#6449=FACE_OUTER_BOUND ( 'NONE', #7463, .T. ) ;
#6451=DIRECTION ( 'NONE',  ( -1.000000000000000000, 0.000000000000000000, 0.000000000000000000 ) ) ;
#6460=CARTESIAN_POINT ( 'NONE',  ( -4.000000000000000000, 0.8576368993457507139, -3.433240632782198709 ) ) ;
#6465=CARTESIAN_POINT ( 'NONE',  ( 4.000000000000000000, -2.309401076758514915, -3.433295621305383349 ) ) ;
#6469=EDGE_CURVE ( 'NONE', #5040, #1717, #144, .T. ) ;
#6471=CARTESIAN_POINT ( 'NONE',  ( -1.390230914382372118, -4.043987460488664532, -3.502507215260523665 ) ) ;
#6472=EDGE_LOOP ( 'NONE', ( #5031, #6059, #3543, #596 ) ) ;
#6478=ADVANCED_FACE ( 'NONE', ( #7796 ), #3152, .F. ) ;
#6483=EDGE_CURVE ( 'NONE', #6485, #170, #4762, .T. ) ;
#6485=VERTEX_POINT ( 'NONE', #3567 ) ;
#6488=ORIENTED_EDGE ( 'NONE', *, *, #3774, .F. ) ;
#6506=FACE_OUTER_BOUND ( 'NONE', #2353, .T. ) ;
#6518=CARTESIAN_POINT ( 'NONE',  ( 0.000000000000000000, 0.000000000000000000, 0.000000000000000000 ) ) ;
#6547=( NAMED_UNIT ( * ) PLANE_ANGLE_UNIT ( ) SI_UNIT ( $, .RADIAN. ) );
#6548=EDGE_LOOP ( 'NONE', ( #5842, #6886, #10522, #6207 ) ) ;
#6562=CARTESIAN_POINT ( 'NONE',  ( -1.655952806101422814, 3.662737355149034979, -7.623296525288699970E-18 ) ) ;
#6564=DIRECTION ( 'NONE',  ( 1.000000000000000000, 0.000000000000000000, 0.000000000000000000 ) ) ;
#6572=CARTESIAN_POINT ( 'NONE',  ( 4.000000000000000000, 2.309401076758497151, -3.433295621305379353 ) ) ;
#6574=CARTESIAN_POINT ( 'NONE',  ( 0.3461262719736147297, -4.658553426539303821, -3.671615880910379381 ) ) ;
#6588=CARTESIAN_POINT ( 'NONE',  ( -0.6920835326022555245, -4.454600218803899558, -3.597382984111586079 ) ) ;
#6597=CARTESIAN_POINT ( 'NONE',  ( -4.101948962585905356, -2.368261337751088824, -3.681124513963624167 ) ) ;
#6660=CARTESIAN_POINT ( 'NONE',  ( 0.000000000000000000, 0.000000000000000000, 0.000000000000000000 ) ) ;
#6663=CARTESIAN_POINT ( 'NONE',  ( -4.198928548860774157, 0.8158838809860065044, -3.526471437616918170 ) ) ;
#6684=ORIENTED_EDGE ( 'NONE', *, *, #8120, .T. ) ;
#6686=CARTESIAN_POINT ( 'NONE',  ( -3.999999999998910649, -1.658469974638591804, -3.531532913075256186 ) ) ;
#6687=( GEOMETRIC_REPRESENTATION_CONTEXT ( 3 ) GLOBAL_UNCERTAINTY_ASSIGNED_CONTEXT ( ( #6199 ) ) GLOBAL_UNIT_ASSIGNED_CONTEXT ( ( #3838, #3013, #5619 ) ) REPRESENTATION_CONTEXT ( 'NONE', 'WORKASPACE' ) );
#6700=CARTESIAN_POINT ( 'NONE',  ( -2.000000000000006661, 3.464101615137750834, 0.000000000000000000 ) ) ;
#6715=MECHANICAL_DESIGN_GEOMETRIC_PRESENTATION_REPRESENTATION('',(#5307),#307);
#6725=CARTESIAN_POINT ( 'NONE',  ( -4.211140560182196957, 2.431303136016537803, -3.745885042887433514 ) ) ;
#6739=EDGE_LOOP ( 'NONE', ( #416, #393, #6377, #903 ) ) ;
#6767=AXIS2_PLACEMENT_3D ( 'NONE', #3029, #6403, #10475 ) ;
#6775=CARTESIAN_POINT ( 'NONE',  ( 2.100000000000000089, 0.000000000000000000, -5.000000000000000000 ) ) ;
#6793=ORIENTED_EDGE ( 'NONE', *, *, #5666, .T. ) ;
#6796=CARTESIAN_POINT ( 'NONE',  ( 2.000000000000005329, -3.464101615137751722, 0.000000000000000000 ) ) ;
#6812=CARTESIAN_POINT ( 'NONE',  ( 0.000000000000000000, 0.000000000000000000, -5.000000000000000888 ) ) ;
#6818=CARTESIAN_POINT ( 'NONE',  ( -2.100000000000000089, 2.571758278209441957E-16, -4.694516984716113228 ) ) ;
#6831=EDGE_CURVE ( 'NONE', #9793, #10907, #805, .T. ) ;
#6836=AXIS2_PLACEMENT_3D ( 'NONE', #5698, #5803, #9867 ) ;
#6848=CIRCLE ( 'NONE', #9872, 0.5155456020628804703 ) ;
#6858=CARTESIAN_POINT ( 'NONE',  ( -4.000000000000000888, -1.539600717839011201, -3.300726591567081591 ) ) ;
#6864=CARTESIAN_POINT ( 'NONE',  ( 1.567478505476135000E-15, 4.618802153517012954, -3.504269196027527844 ) ) ;
#6879=ADVANCED_FACE ( 'NONE', ( #3989, #10825 ), #3209, .T. ) ;
#6882=EDGE_CURVE ( 'NONE', #3061, #4045, #2006, .T. ) ;
#6886=ORIENTED_EDGE ( 'NONE', *, *, #7702, .T. ) ;
#6891=DIRECTION ( 'NONE',  ( -1.000000000000000000, 0.000000000000000000, 0.000000000000000000 ) ) ;
#6898=EDGE_CURVE ( 'NONE', #7216, #3459, #5401, .T. ) ;
#6903=CARTESIAN_POINT ( 'NONE',  ( -4.000000000000000000, -2.309401076758515803, -0.4999999999999995559 ) ) ;
#6920=CARTESIAN_POINT ( 'NONE',  ( 4.175002511812151873, 2.208363329454889445, -3.469254087858244073 ) ) ;
#6923=CARTESIAN_POINT ( 'NONE',  ( 2.000000000000005329, -3.464101615137751722, 0.000000000000000000 ) ) ;
#6927=FACE_OUTER_BOUND ( 'NONE', #4411, .T. ) ;
#6934=VERTEX_POINT ( 'NONE', #6818 ) ;
#6937=DIRECTION ( 'NONE',  ( -0.000000000000000000, -0.000000000000000000, 1.000000000000000000 ) ) ;
#6941=VECTOR ( 'NONE', #7588, 1000.000000000000000 ) ;
#6942=DIRECTION ( 'NONE',  ( -0.000000000000000000, -0.000000000000000000, 1.000000000000000000 ) ) ;
#6943=B_SPLINE_CURVE_WITH_KNOTS ( 'NONE', 3,
 ( #7621, #2454, #6663, #2627, #9222, #6725 ),
 .UNSPECIFIED., .F., .F.,
 ( 4, 2, 4 ),
 ( 0.002452478801916376308, 0.003676905084148007850, 0.004901331366379639391 ),
 .UNSPECIFIED. ) ;
#6956=CARTESIAN_POINT ( 'NONE',  ( 0.000000000000000000, 0.000000000000000000, 0.000000000000000000 ) ) ;
#6978=DIRECTION ( 'NONE',  ( -1.000000000000000000, 0.000000000000000000, 0.000000000000000000 ) ) ;
#6984=CARTESIAN_POINT ( 'NONE',  ( 0.000000000000000000, 0.000000000000000000, -25.03750572909317285 ) ) ;
#6993=SHAPE_DEFINITION_REPRESENTATION ( #3849, #6402 ) ;
#6997=DIRECTION ( 'NONE',  ( -0.9396926207859138680, 0.000000000000000000, -0.3420201433256536139 ) ) ;
#6999=AXIS2_PLACEMENT_3D ( 'NONE', #10772, #5830, #2326 ) ;
#7010=CLOSED_SHELL ( 'NONE', ( #8664, #6478, #7690, #4742, #3040, #5568, #10473, #7525, #5794, #7156, #4721, #2266, #581, #2001, #6879, #10239, #9936, #709, #2771, #2716, #2699, #5849, #8860, #3248, #10688, #4656, #3361, #4047, #2573, #4600, #9333, #4535 ) ) ;
#7013=CARTESIAN_POINT ( 'NONE',  ( 2.000000000000008882, 3.464101615137749945, 0.000000000000000000 ) ) ;
#7025=ORIENTED_EDGE ( 'NONE', *, *, #572, .T. ) ;
#7029=CIRCLE ( 'NONE', #1162, 4.000000000000000000 ) ;
#7079=CARTESIAN_POINT ( 'NONE',  ( -3.680118525130244400, 2.494084732383327285, -0.3507732604232449702 ) ) ;
#7081=ORIENTED_EDGE ( 'NONE', *, *, #5685, .F. ) ;
#7133=CARTESIAN_POINT ( 'NONE',  ( 1.999999999999998224, -3.464101615137772594, -3.142992957459239012 ) ) ;
#7137=CARTESIAN_POINT ( 'NONE',  ( 1.411581201560190495E-15, 4.862606272033091592, -3.745885042887436622 ) ) ;
#7141=CARTESIAN_POINT ( 'NONE',  ( 4.204015924366189871, -1.626724848190933548, -3.610627190413393084 ) ) ;
#7156=ADVANCED_FACE ( 'NONE', ( #10378 ), #8712, .F. ) ;
#7157=CARTESIAN_POINT ( 'NONE',  ( -0.6666666666666666297, -4.233901974057276973, -3.300726591567087365 ) ) ;
#7187=DIRECTION ( 'NONE',  ( 0.000000000000000000, 0.000000000000000000, -1.000000000000000000 ) ) ;
#7216=VERTEX_POINT ( 'NONE', #8828 ) ;
#7238=CARTESIAN_POINT ( 'NONE',  ( 4.000000000000000000, 0.000000000000000000, 0.000000000000000000 ) ) ;
#7259=CARTESIAN_POINT ( 'NONE',  ( -1.274258131565027874, -3.883108878240886241, -3.220599429844051009 ) ) ;
#7261=DIRECTION ( 'NONE',  ( 0.8191520442889902442, 1.003171929053522651E-16, -0.5735764363510482688 ) ) ;
#7274=( NAMED_UNIT ( * ) SI_UNIT ( $, .STERADIAN. ) SOLID_ANGLE_UNIT ( ) );
#7291=CARTESIAN_POINT ( 'NONE',  ( 4.000000000000000000, 0.000000000000000000, 0.000000000000000000 ) ) ;
#7294=UNCERTAINTY_MEASURE_WITH_UNIT (LENGTH_MEASURE( 1.000000000000000082E-05 ), #5535, 'distance_accuracy_value', 'NONE');
#7320=VERTEX_POINT ( 'NONE', #9980 ) ;
#7324=CARTESIAN_POINT ( 'NONE',  ( -3.861362476283256129, -2.629030857716004199, -3.671615880910374941 ) ) ;
#7335=EDGE_CURVE ( 'NONE', #8932, #7431, #4269, .T. ) ;
#7372=AXIS2_PLACEMENT_3D ( 'NONE', #9909, #10681, #3954 ) ;
#7387=CARTESIAN_POINT ( 'NONE',  ( 0.6640947660595348800, -4.471078309994175548, -3.602146406945708090 ) ) ;
#7391=CARTESIAN_POINT ( 'NONE',  ( -2.500000000000000888, 0.000000000000000000, -4.974599999999998801 ) ) ;
#7393=STYLED_ITEM ( 'NONE', ( #2224 ), #10767 ) ;
#7401=CARTESIAN_POINT ( 'NONE',  ( -2.000000000000006661, 3.464101615137750834, 0.000000000000000000 ) ) ;
#7418=CARTESIAN_POINT ( 'NONE',  ( 4.197478902586992966, -0.8524102783748346290, -3.505063281295504041 ) ) ;
#7431=VERTEX_POINT ( 'NONE', #6378 ) ;
#7441=CARTESIAN_POINT ( 'NONE',  ( -4.000000000000000000, 0.3987449864459974846, -0.01220643443059782861 ) ) ;
#7449=B_SPLINE_CURVE_WITH_KNOTS ( 'NONE', 3,
 ( #245, #142, #4438, #1867, #4376, #4318, #7706, #5209 ),
 .UNSPECIFIED., .F., .F.,
 ( 4, 2, 2, 4 ),
 ( 2.465131517071610173E-07, 0.001183067374689837636, 0.001774477805458902699, 0.002365888236227967761 ),
 .UNSPECIFIED. ) ;
#7463=EDGE_LOOP ( 'NONE', ( #4306, #8840, #8050 ) ) ;
#7489=CARTESIAN_POINT ( 'NONE',  ( 4.211140560182196957, -2.431303136016555122, -3.745885042887436622 ) ) ;
#7491=EDGE_CURVE ( 'NONE', #4045, #1489, #4802, .T. ) ;
#7496=CARTESIAN_POINT ( 'NONE',  ( -4.000000000000000888, 1.563622288139195238, -0.2253451193528307472 ) ) ;
#7506=VERTEX_POINT ( 'NONE', #6700 ) ;
#7514=DIRECTION ( 'NONE',  ( -1.000000000000000000, 0.000000000000000000, 0.000000000000000000 ) ) ;
#7525=ADVANCED_FACE ( 'NONE', ( #5003 ), #493, .T. ) ;
#7528=VECTOR ( 'NONE', #1152, 999.9999999999998863 ) ;
#7530=CARTESIAN_POINT ( 'NONE',  ( 4.000000000000000000, -1.700175430507292473, -3.320327275037661785 ) ) ;
#7532=AXIS2_PLACEMENT_3D ( 'NONE', #8144, #3918, #8193 ) ;
#7533=CARTESIAN_POINT ( 'NONE',  ( -4.197393957002303999, -7.773935952363655451E-14, -3.503767560748929810 ) ) ;
#7571=PLANE ( 'NONE',  #1267 ) ;
#7579=EDGE_LOOP ( 'NONE', ( #4998, #6319, #5157, #3299, #7025, #5795, #3055 ) ) ;
#7588=DIRECTION ( 'NONE',  ( 0.000000000000000000, 0.000000000000000000, 1.000000000000000000 ) ) ;
#7603=CARTESIAN_POINT ( 'NONE',  ( -4.000000000000000000, 2.309401076758498483, -5.000000000000000000 ) ) ;
#7611=CARTESIAN_POINT ( 'NONE',  ( 0.000000000000000000, 0.000000000000000000, -0.3080913168122742518 ) ) ;
#7612=ORIENTED_EDGE ( 'NONE', *, *, #6147, .F. ) ;
#7615=CARTESIAN_POINT ( 'NONE',  ( -4.000000000000000000, 0.9868501483902560878, -0.09357334158579519445 ) ) ;
#7621=CARTESIAN_POINT ( 'NONE',  ( -4.197393957002303999, -7.773935952363655451E-14, -3.503767560748929810 ) ) ;
#7640=CARTESIAN_POINT ( 'NONE',  ( 1.655952806101427033, -3.662737355149048302, -1.182683869819604841E-14 ) ) ;
#7644=CARTESIAN_POINT ( 'NONE',  ( 0.5636800770130377947, 4.293361309317166530, -3.531542292954102713 ) ) ;
#7648=CARTESIAN_POINT ( 'NONE',  ( 3.679171394226031122, 2.494631558665830973, -0.3503314178412474389 ) ) ;
#7652=LINE ( 'NONE', #5044, #4428 ) ;
#7674=CARTESIAN_POINT ( 'NONE',  ( -4.000000000000000000, -2.309401076758515803, -0.4999999999999995559 ) ) ;
#7675=CARTESIAN_POINT ( 'NONE',  ( 8.673617379884035472E-16, 4.618802153517012954, 0.000000000000000000 ) ) ;
#7690=ADVANCED_FACE ( 'NONE', ( #1889 ), #1140, .F. ) ;
#7702=EDGE_CURVE ( 'NONE', #3831, #1419, #2209, .T. ) ;
#7706=CARTESIAN_POINT ( 'NONE',  ( 2.171643655288379993, -3.365003104552334978, -1.195831703456429434E-14 ) ) ;
#7751=ORIENTED_EDGE ( 'NONE', *, *, #9114, .F. ) ;
#7757=CARTESIAN_POINT ( 'NONE',  ( -6.259644161404860030E-16, -4.618802153517027165, -5.000000000000000000 ) ) ;
#7774=AXIS2_PLACEMENT_3D ( 'NONE', #8621, #1377, #4409 ) ;
#7786=CARTESIAN_POINT ( 'NONE',  ( 4.211140560182196957, 2.431303136016536470, -3.745885042887433514 ) ) ;
#7796=FACE_OUTER_BOUND ( 'NONE', #6472, .T. ) ;
#7798=CIRCLE ( 'NONE', #1221, 4.000000000000000000 ) ;
#7820=DIRECTION ( 'NONE',  ( -0.000000000000000000, 0.000000000000000000, -1.000000000000000000 ) ) ;
#7845=VERTEX_POINT ( 'NONE', #8604 ) ;
#7847=VERTEX_POINT ( 'NONE', #159 ) ;
#7849=EDGE_LOOP ( 'NONE', ( #5615, #10800, #3902, #5743 ) ) ;
#7857=CARTESIAN_POINT ( 'NONE',  ( -2.687328764639638656, 3.067272167851286202, -0.05923475698270370959 ) ) ;
#7868=CARTESIAN_POINT ( 'NONE',  ( 1.274258131564866448, 3.883108878240963513, -3.220599429844046568 ) ) ;
#7874=DIRECTION ( 'NONE',  ( 0.000000000000000000, 0.000000000000000000, 1.000000000000000000 ) ) ;
#7879=DIRECTION ( 'NONE',  ( -0.000000000000000000, -0.000000000000000000, 1.000000000000000000 ) ) ;
#7890=CARTESIAN_POINT ( 'NONE',  ( -6.259644161404860030E-16, -4.618802153517027165, -3.433295621305388234 ) ) ;
#7912=CARTESIAN_POINT ( 'NONE',  ( -4.000000000000000000, 2.309401076758498483, -3.433295621305379353 ) ) ;
#7925=FACE_OUTER_BOUND ( 'NONE', #2872, .T. ) ;
#7940=ORIENTED_EDGE ( 'NONE', *, *, #9790, .F. ) ;
#7950=ORIENTED_EDGE ( 'NONE', *, *, #7491, .T. ) ;
#7952=VERTEX_POINT ( 'NONE', #2111 ) ;
#7982=SURFACE_SIDE_STYLE ('',( #6246 ) ) ;
#7998=EDGE_CURVE ( 'NONE', #3058, #170, #5500, .T. ) ;
#8014=CARTESIAN_POINT ( 'NONE',  ( 4.211140560182196957, 2.431303136016536470, -3.745885042887433514 ) ) ;
#8021=ORIENTED_EDGE ( 'NONE', *, *, #3905, .T. ) ;
#8035=VECTOR ( 'NONE', #7261, 1000.000000000000114 ) ;
#8050=ORIENTED_EDGE ( 'NONE', *, *, #3317, .F. ) ;
#8078=DIRECTION ( 'NONE',  ( 0.000000000000000000, 0.000000000000000000, -1.000000000000000000 ) ) ;
#8095=CARTESIAN_POINT ( 'NONE',  ( -2.836893136758495970, -3.208949435745868328, -3.505054077164885484 ) ) ;
#8106=VERTEX_POINT ( 'NONE', #6923 ) ;
#8111=ORIENTED_EDGE ( 'NONE', *, *, #2396, .T. ) ;
#8120=EDGE_CURVE ( 'NONE', #12, #4811, #933, .T. ) ;
#8123=AXIS2_PLACEMENT_3D ( 'NONE', #3623, #3733, #6339 ) ;
#8138=EDGE_CURVE ( 'NONE', #8106, #7431, #3470, .T. ) ;
#8140=( NAMED_UNIT ( * ) SI_UNIT ( $, .STERADIAN. ) SOLID_ANGLE_UNIT ( ) );
#8143=CARTESIAN_POINT ( 'NONE',  ( -4.204114297095464359, 1.660363174096617156, -3.602136431857887011 ) ) ;
#8144=CARTESIAN_POINT ( 'NONE',  ( 0.000000000000000000, 0.000000000000000000, 0.000000000000000000 ) ) ;
#8145=B_SPLINE_CURVE_WITH_KNOTS ( 'NONE', 3,
 ( #4475, #7079, #10520, #3847, #7857, #4580, #1176, #1293 ),
 .UNSPECIFIED., .F., .F.,
 ( 4, 2, 2, 4 ),
 ( 2.465131517071352357E-07, 0.001183067374689843057, 0.001774477805458910071, 0.002365888236227977302 ),
 .UNSPECIFIED. ) ;
#8152=LINE ( 'NONE', #10337, #8035 ) ;
#8169=CARTESIAN_POINT ( 'NONE',  ( 3.455068668934414777, -2.624017327439094327, -3.316620875263732504 ) ) ;
#8179=EDGE_CURVE ( 'NONE', #12, #10561, #1090, .T. ) ;
#8193=DIRECTION ( 'NONE',  ( -1.000000000000000000, 0.000000000000000000, 0.000000000000000000 ) ) ;
#8195=CARTESIAN_POINT ( 'NONE',  ( -0.5276280594146446346, 4.314175951381965746, -3.320322319201721495 ) ) ;
#8197=CARTESIAN_POINT ( 'NONE',  ( 3.511755186886750923, -2.826662030176382956, -3.597382984111582083 ) ) ;
#8216=CARTESIAN_POINT ( 'NONE',  ( -0.1404048886732797152, -4.699864953788083888, -3.686887068327043160 ) ) ;
#8221=EDGE_LOOP ( 'NONE', ( #1981, #2172, #9430, #2823 ) ) ;
#8242=DIRECTION ( 'NONE',  ( -0.000000000000000000, -0.000000000000000000, 1.000000000000000000 ) ) ;
#8249=CARTESIAN_POINT ( 'NONE',  ( 2.805705207896068476, -3.226868319750173075, -3.503898532754370354 ) ) ;
#8250=CARTESIAN_POINT ( 'NONE',  ( 3.999999999999998224, 2.472263674411418588, -3.687027874309861897 ) ) ;
#8269=EDGE_LOOP ( 'NONE', ( #1079, #184 ) ) ;
#8272=ORIENTED_EDGE ( 'NONE', *, *, #8179, .F. ) ;
#8283=ORIENTED_EDGE ( 'NONE', *, *, #10711, .T. ) ;
#8288=CARTESIAN_POINT ( 'NONE',  ( -1.317756351988340180, 3.857995168970202116, -0.04852650426601388955 ) ) ;
#8292=ORIENTED_EDGE ( 'NONE', *, *, #3597, .T. ) ;
#8293=DIRECTION ( 'NONE',  ( -0.8660254037844373753, 0.5000000000000021094, 0.000000000000000000 ) ) ;
#8298=CARTESIAN_POINT ( 'NONE',  ( -4.000000000000000000, 2.471528634177585282, -3.686887442155186712 ) ) ;
#8322=VERTEX_POINT ( 'NONE', #8440 ) ;
#8324=ORIENTED_EDGE ( 'NONE', *, *, #2477, .F. ) ;
#8333=CARTESIAN_POINT ( 'NONE',  ( 4.000000000000000000, -2.309401076758516691, -0.4999999999999995559 ) ) ;
#8344=CARTESIAN_POINT ( 'NONE',  ( -0.6507732100473471171, 4.243078065514775510, -0.2236248678334823436 ) ) ;
#8351=CARTESIAN_POINT ( 'NONE',  ( 0.6507732100473444525, -4.243078065514795050, -0.2236248678334952777 ) ) ;
#8353=CARTESIAN_POINT ( 'NONE',  ( -4.000000000000000000, -0.8232339106130515116, -3.430630286862743183 ) ) ;
#8355=CARTESIAN_POINT ( 'NONE',  ( 4.203833317240879275, 1.627343821129582979, -3.597273115243889929 ) ) ;
#8358=CARTESIAN_POINT ( 'NONE',  ( -5.560781378645575757, 6.809993116116508640E-16, -4.000000000000000000 ) ) ;
#8360=AXIS2_PLACEMENT_3D ( 'NONE', #1629, #5026, #8398 ) ;
#8373=ORIENTED_EDGE ( 'NONE', *, *, #9322, .T. ) ;
#8398=DIRECTION ( 'NONE',  ( 1.000000000000000000, 0.000000000000000000, 0.000000000000000000 ) ) ;
#8415=CARTESIAN_POINT ( 'NONE',  ( 4.211399257449709665, -2.459727064652517114, -3.751161691472417736 ) ) ;
#8428=AXIS2_PLACEMENT_3D ( 'NONE', #9831, #6388, #6433 ) ;
#8429=ORIENTED_EDGE ( 'NONE', *, *, #2031, .T. ) ;
#8430=EDGE_CURVE ( 'NONE', #990, #7845, #2413, .T. ) ;
#8440=CARTESIAN_POINT ( 'NONE',  ( 2.500000000000000444, 0.000000000000000000, -5.000000000000000888 ) ) ;
#8446=DIRECTION ( 'NONE',  ( -0.000000000000000000, 0.000000000000000000, -1.000000000000000000 ) ) ;
#8462=PRODUCT_DEFINITION_FORMATION_WITH_SPECIFIED_SOURCE ( 'ANY', '', #9880, .NOT_KNOWN. ) ;
#8467=EDGE_LOOP ( 'NONE', ( #6488, #3322 ) ) ;
#8470=CARTESIAN_POINT ( 'NONE',  ( 0.000000000000000000, 0.000000000000000000, -4.000000000000000000 ) ) ;
#8481=CARTESIAN_POINT ( 'NONE',  ( -4.211140560182196957, -2.431303136016552013, -3.745885042887436178 ) ) ;
#8497=CARTESIAN_POINT ( 'NONE',  ( 0.000000000000000000, 0.000000000000000000, -4.974599999999998801 ) ) ;
#8503=CARTESIAN_POINT ( 'NONE',  ( -2.682243648011671588, -3.070208061305317759, -0.04852650426602272971 ) ) ;
#8504=LINE ( 'NONE', #6775, #3535 ) ;
#8509=( BOUNDED_SURFACE ( )  B_SPLINE_SURFACE ( 3, 2, ( 
 ( #2999, #10700, #6376 ),
 ( #1316, #5546, #3094 ),
 ( #8927, #4714, #8095 ),
 ( #7259, #5597, #6471 ),
 ( #2260, #10654, #3044 ),
 ( #5655, #1427, #6418 ) ),
 .UNSPECIFIED., .F., .F., .F. ) 
 B_SPLINE_SURFACE_WITH_KNOTS ( ( 4, 2, 4 ),
 ( 3, 3 ),
 ( 0.02032853247518126918, 0.02278863295364821906, 0.02524873343211516893 ),
 ( 0.000000000000000000, 1.000000000000000000 ),
 .UNSPECIFIED. ) 
 GEOMETRIC_REPRESENTATION_ITEM ( )  RATIONAL_B_SPLINE_SURFACE ( (
 ( 1.000000000000000000, 0.8047781615896838492, 1.000000000000000000),
 ( 1.000000000000000000, 0.8123767586288186404, 1.000000000000000000),
 ( 1.000000000000000000, 0.8190662415565814758, 1.000000000000000000),
 ( 1.000000000000000000, 0.8192361015667604107, 1.000000000000000000),
 ( 1.000000000000000000, 0.8126135807104967190, 1.000000000000000000),
 ( 1.000000000000000000, 0.8047712338318580017, 1.000000000000000000) ) ) 
 REPRESENTATION_ITEM ( '' )  SURFACE ( )  );
#8513=ORIENTED_EDGE ( 'NONE', *, *, #2889, .F. ) ;
#8523=CARTESIAN_POINT ( 'NONE',  ( 2.499999999999999556, 0.000000000000000000, 3.469446951953614189E-15 ) ) ;
#8530=CARTESIAN_POINT ( 'NONE',  ( -4.000000000000000000, 2.309401076758498483, -3.433295621305379353 ) ) ;
#8533=DIRECTION ( 'NONE',  ( 0.000000000000000000, -1.000000000000000000, 0.000000000000000000 ) ) ;
#8539=CARTESIAN_POINT ( 'NONE',  ( -4.197393957002303999, -0.8151795401431414234, -3.503767560748935139 ) ) ;
#8576=VERTEX_POINT ( 'NONE', #5608 ) ;
#8578=DIRECTION ( 'NONE',  ( 0.000000000000000000, 0.000000000000000000, -1.000000000000000000 ) ) ;
#8597=DIRECTION ( 'NONE',  ( -0.000000000000000000, -0.000000000000000000, 1.000000000000000000 ) ) ;
#8599=ORIENTED_EDGE ( 'NONE', *, *, #4908, .F. ) ;
#8601=ORIENTED_EDGE ( 'NONE', *, *, #225, .T. ) ;
#8604=CARTESIAN_POINT ( 'NONE',  ( -6.259644161404860030E-16, -4.618802153517027165, -3.433295621305388234 ) ) ;
#8608=CARTESIAN_POINT ( 'NONE',  ( 1.391697335622810172, 4.043246145443375461, -3.503898532754365913 ) ) ;
#8612=CONICAL_SURFACE ( 'NONE', #1876, 5.560781378645573980, 1.221730476396046816 ) ;
#8621=CARTESIAN_POINT ( 'NONE',  ( 0.000000000000000000, 0.000000000000000000, -4.000000000000000000 ) ) ;
#8662=ORIENTED_EDGE ( 'NONE', *, *, #1583, .T. ) ;
#8663=CARTESIAN_POINT ( 'NONE',  ( 4.000000000000000000, 2.309401076758497151, -5.000000000000000000 ) ) ;
#8664=ADVANCED_FACE ( 'NONE', ( #1986 ), #5373, .F. ) ;
#8712=PLANE ( 'NONE',  #4870 ) ;
#8746=CARTESIAN_POINT ( 'NONE',  ( 1.390230914382191596, 4.043987460488659202, -3.502507215260488582 ) ) ;
#8753=DIRECTION ( 'NONE',  ( -0.000000000000000000, -0.000000000000000000, 1.000000000000000000 ) ) ;
#8754=B_SPLINE_CURVE_WITH_KNOTS ( 'NONE', 3,
 ( #9692, #557, #3075, #3955, #6448, #8804 ),
 .UNSPECIFIED., .F., .F.,
 ( 4, 2, 4 ),
 ( 0.000000000000000000, 0.0002095117440854740156, 0.0004190234881709480313 ),
 .UNSPECIFIED. ) ;
#8770=CARTESIAN_POINT ( 'NONE',  ( -3.333333333333332149, -2.694301256218264218, -3.300726591567082036 ) ) ;
#8781=ORIENTED_EDGE ( 'NONE', *, *, #2559, .F. ) ;
#8800=( BOUNDED_SURFACE ( )  B_SPLINE_SURFACE ( 3, 2, ( 
 ( #4924, #8298, #8920 ),
 ( #1366, #4765, #8143 ),
 ( #3086, #6460, #5648 ),
 ( #5912, #8353, #3305 ),
 ( #5033, #6686, #2650 ),
 ( #732, #1809, #16 ) ),
 .UNSPECIFIED., .F., .F., .F. ) 
 B_SPLINE_SURFACE_WITH_KNOTS ( ( 4, 2, 4 ),
 ( 3, 3 ),
 ( 0.02027752710269158445, 0.02273781595091097299, 0.02519810479913036153 ),
 ( 0.000000000000000000, 1.000000000000000000 ),
 .UNSPECIFIED. ) 
 GEOMETRIC_REPRESENTATION_ITEM ( )  RATIONAL_B_SPLINE_SURFACE ( (
 ( 1.000000000000000000, 0.8047781431712808242, 1.000000000000000000),
 ( 1.000000000000000000, 0.8123773247083928561, 1.000000000000000000),
 ( 1.000000000000000000, 0.8190670192154906326, 1.000000000000000000),
 ( 1.000000000000000000, 0.8192353552912178261, 1.000000000000000000),
 ( 1.000000000000000000, 0.8126132098226825917, 1.000000000000000000),
 ( 1.000000000000000000, 0.8047712465856394770, 1.000000000000000000) ) ) 
 REPRESENTATION_ITEM ( '' )  SURFACE ( )  );
#8804=CARTESIAN_POINT ( 'NONE',  ( -6.473970235329672780E-16, -4.862606272033106691, -3.745885042887442395 ) ) ;
#8814=CIRCLE ( 'NONE', #9699, 2.500000000000000888 ) ;
#8828=CARTESIAN_POINT ( 'NONE',  ( 2.500000000000000888, 3.061616997868384127E-16, -4.974599999999998801 ) ) ;
#8834=CARTESIAN_POINT ( 'NONE',  ( 1.567478505476134606E-15, 4.618802153517012066, -3.433295621305382905 ) ) ;
#8840=ORIENTED_EDGE ( 'NONE', *, *, #1888, .T. ) ;
#8841=AXIS2_PLACEMENT_3D ( 'NONE', #3343, #10120, #171 ) ;
#8860=ADVANCED_FACE ( 'NONE', ( #8978 ), #963, .T. ) ;
#8868=DIRECTION ( 'NONE',  ( 0.000000000000000000, -0.000000000000000000, 1.000000000000000000 ) ) ;
#8878=CARTESIAN_POINT ( 'NONE',  ( -4.141042297810615835, 2.227970268150415656, -3.687027686973619822 ) ) ;
#8880=CARTESIAN_POINT ( 'NONE',  ( 5.384454397937118664, 0.000000000000000000, -5.000000000000000000 ) ) ;
#8892=ORIENTED_EDGE ( 'NONE', *, *, #6469, .F. ) ;
#8898=CARTESIAN_POINT ( 'NONE',  ( 1.360585162435110629, -4.061296242128317857, -3.505054077164905024 ) ) ;
#8900=AXIS2_PLACEMENT_3D ( 'NONE', #5789, #4013, #3956 ) ;
#8902=DIRECTION ( 'NONE',  ( 0.9396926207859138680, 1.150791560227856926E-16, -0.3420201433256536139 ) ) ;
#8905=EDGE_LOOP ( 'NONE', ( #1712, #5305, #435, #10108 ) ) ;
#8920=CARTESIAN_POINT ( 'NONE',  ( -4.211399284164270895, 2.459729995988205964, -3.751162237960538715 ) ) ;
#8927=CARTESIAN_POINT ( 'NONE',  ( -2.756197834950067094, -3.027510591568735254, -3.223146290109809797 ) ) ;
#8930=CARTESIAN_POINT ( 'NONE',  ( -0.3198814748697807464, -4.434118497892185040, -0.3507732604232532969 ) ) ;
#8932=VERTEX_POINT ( 'NONE', #1810 ) ;
#8978=FACE_OUTER_BOUND ( 'NONE', #4157, .T. ) ;
#8979=FACE_OUTER_BOUND ( 'NONE', #4911, .T. ) ;
#8980=CARTESIAN_POINT ( 'NONE',  ( -0.6640947660597427138, 4.471078309994878985, -3.602146406945963442 ) ) ;
#8982=CARTESIAN_POINT ( 'NONE',  ( 1.828356344711641102, 3.563200125723180900, -5.433716356636336675E-16 ) ) ;
#8985=CARTESIAN_POINT ( 'NONE',  ( 0.000000000000000000, 0.000000000000000000, 0.000000000000000000 ) ) ;
#9030=DIRECTION ( 'NONE',  ( -0.000000000000000000, -0.000000000000000000, 1.000000000000000000 ) ) ;
#9037=EDGE_LOOP ( 'NONE', ( #3566, #8021, #8892, #2697 ) ) ;
#9053=CARTESIAN_POINT ( 'NONE',  ( 4.236525694536557474, -2.416953475386482530, -3.751298745799839462 ) ) ;
#9059=EDGE_LOOP ( 'NONE', ( #2051, #9205, #5827, #1719 ) ) ;
#9064=AXIS2_PLACEMENT_3D ( 'NONE', #5152, #8533, #2186 ) ;
#9106=CARTESIAN_POINT ( 'NONE',  ( 4.000000000000000000, -1.942223658245635809, -0.3516579909967643691 ) ) ;
#9114=EDGE_CURVE ( 'NONE', #7847, #3283, #5891, .T. ) ;
#9122=CARTESIAN_POINT ( 'NONE',  ( 4.000000000000000000, 2.309401076758497151, -5.000000000000000000 ) ) ;
#9136=CARTESIAN_POINT ( 'NONE',  ( 4.211405965630455661, 2.460463115436283932, -3.751298928144577882 ) ) ;
#9153=CARTESIAN_POINT ( 'NONE',  ( -4.211140560182196957, -2.431303136016552013, -3.745885042887436178 ) ) ;
#9170=VERTEX_POINT ( 'NONE', #7238 ) ;
#9180=CARTESIAN_POINT ( 'NONE',  ( 0.000000000000000000, 0.000000000000000000, 0.000000000000000000 ) ) ;
#9187=CARTESIAN_POINT ( 'NONE',  ( 4.000000000000000000, 2.309401076758497151, -3.433295621305379353 ) ) ;
#9192=EDGE_CURVE ( 'NONE', #4635, #6934, #2388, .T. ) ;
#9193=CARTESIAN_POINT ( 'NONE',  ( 1.312671235360372224, 3.860931062424219462, -0.05923475698270440348 ) ) ;
#9195=CARTESIAN_POINT ( 'NONE',  ( 4.000000000000000000, -1.677850389431204459, -3.535268758346977513 ) ) ;
#9200=CARTESIAN_POINT ( 'NONE',  ( 5.560781378645575757, 0.000000000000000000, -4.000000000000000000 ) ) ;
#9205=ORIENTED_EDGE ( 'NONE', *, *, #10410, .T. ) ;
#9207=ORIENTED_EDGE ( 'NONE', *, *, #8138, .F. ) ;
#9222=CARTESIAN_POINT ( 'NONE',  ( -4.207491450040567571, 2.029819825146470524, -3.671670828759566074 ) ) ;
#9247=CARTESIAN_POINT ( 'NONE',  ( 4.000000000000000888, 0.8228435280416209752, -3.430609588141487976 ) ) ;
#9275=CARTESIAN_POINT ( 'NONE',  ( 3.999999999999999112, 1.941961291383486277, -0.3515519931180248192 ) ) ;
#9311=CARTESIAN_POINT ( 'NONE',  ( -4.000000000000000000, -1.942223658245633811, -0.3516579909967644246 ) ) ;
#9312=VECTOR ( 'NONE', #3600, 1000.000000000000000 ) ;
#9322=EDGE_CURVE ( 'NONE', #1489, #1717, #3610, .T. ) ;
#9333=ADVANCED_FACE ( 'NONE', ( #10385 ), #4715, .F. ) ;
#9334=DIRECTION ( 'NONE',  ( 0.000000000000000000, 0.000000000000000000, 1.000000000000000000 ) ) ;
#9358=CARTESIAN_POINT ( 'NONE',  ( -3.999999999999999112, 1.539600717838996324, -3.300726591567078039 ) ) ;
#9363=CARTESIAN_POINT ( 'NONE',  ( 4.140404888673277384, 2.228338276487440428, -3.686887068327033390 ) ) ;
#9375=CIRCLE ( 'NONE', #6182, 2.500000000000000444 ) ;
#9399=EDGE_CURVE ( 'NONE', #4773, #4811, #10403, .T. ) ;
#9430=ORIENTED_EDGE ( 'NONE', *, *, #4908, .T. ) ;
#9469=CARTESIAN_POINT ( 'NONE',  ( 0.5449313310647804220, 4.304185902836899835, -3.316620875263383894 ) ) ;
#9477=CARTESIAN_POINT ( 'NONE',  ( 4.197393957002303999, -0.4069871074557456780, -3.503767560748925813 ) ) ;
#9482=DIRECTION ( 'NONE',  ( -1.000000000000000000, 0.000000000000000000, 0.000000000000000000 ) ) ;
#9483=CARTESIAN_POINT ( 'NONE',  ( -6.473970235329672780E-16, -4.862606272033106691, -3.745885042887442395 ) ) ;
#9494=VECTOR ( 'NONE', #8902, 1000.000000000000227 ) ;
#9529=CARTESIAN_POINT ( 'NONE',  ( 1.567478505476134606E-15, 4.618802153517012066, -3.433295621305382905 ) ) ;
#9531=ORIENTED_EDGE ( 'NONE', *, *, #225, .F. ) ;
#9539=EDGE_CURVE ( 'NONE', #9793, #38, #2541, .T. ) ;
#9561=EDGE_LOOP ( 'NONE', ( #7081, #6274, #9207, #4450, #8429, #7940 ) ) ;
#9565=DIRECTION ( 'NONE',  ( 1.000000000000000000, 0.000000000000000000, 0.000000000000000000 ) ) ;
#9578=CARTESIAN_POINT ( 'NONE',  ( -0.02511973781850462134, 4.877415612947412882, -3.751298745799839462 ) ) ;
#9583=DIRECTION ( 'NONE',  ( -1.000000000000000000, 0.000000000000000000, 0.000000000000000000 ) ) ;
#9612=B_SPLINE_CURVE_WITH_KNOTS ( 'NONE', 3,
 ( #4981, #8355, #734, #1423 ),
 .UNSPECIFIED., .F., .F.,
 ( 4, 4 ),
 ( 0.000000000000000000, 0.002452478801916361129 ),
 .UNSPECIFIED. ) ;
#9616=EDGE_CURVE ( 'NONE', #6444, #7847, #6419, .T. ) ;
#9621=CARTESIAN_POINT ( 'NONE',  ( -4.154094228333456762, 2.398367420968013253, -3.721909803043220055 ) ) ;
#9632=DIRECTION ( 'NONE',  ( 1.000000000000000000, 0.000000000000000000, 0.000000000000000000 ) ) ;
#9645=CARTESIAN_POINT ( 'NONE',  ( -4.000000000000000000, 0.000000000000000000, 0.000000000000000000 ) ) ;
#9655=EDGE_LOOP ( 'NONE', ( #3553, #5280, #2681 ) ) ;
#9690=CIRCLE ( 'NONE', #10404, 2.499999999999999556 ) ;
#9692=CARTESIAN_POINT ( 'NONE',  ( -6.259644161404860030E-16, -4.618802153517027165, -3.433295621305388234 ) ) ;
#9697=ORIENTED_EDGE ( 'NONE', *, *, #2080, .F. ) ;
#9699=AXIS2_PLACEMENT_3D ( 'NONE', #8497, #5995, #878 ) ;
#9703=DIRECTION ( 'NONE',  ( 1.000000000000000000, 0.000000000000000000, 0.000000000000000000 ) ) ;
#9704=CARTESIAN_POINT ( 'NONE',  ( -4.000000000000000000, -1.560351142792950618, -0.2242961665059814425 ) ) ;
#9705=CARTESIAN_POINT ( 'NONE',  ( 0.1750025118121568690, 4.719839900820621104, -3.469254087858248070 ) ) ;
#9767=CARTESIAN_POINT ( 'NONE',  ( -1.144235203016679359, -3.958177651039096911, -0.09382832055446428676 ) ) ;
#9786=AXIS2_PLACEMENT_3D ( 'NONE', #316, #8597, #10267 ) ;
#9790=EDGE_CURVE ( 'NONE', #7506, #10481, #7029, .T. ) ;
#9793=VERTEX_POINT ( 'NONE', #6465 ) ;
#9801=CARTESIAN_POINT ( 'NONE',  ( 4.000000000000000888, 1.563622288139206118, -0.2253451193528334950 ) ) ;
#9809=FACE_OUTER_BOUND ( 'NONE', #9059, .T. ) ;
#9813=FACE_OUTER_BOUND ( 'NONE', #8905, .T. ) ;
#9815=CARTESIAN_POINT ( 'NONE',  ( 0.6448876103708359731, 4.246476118072354922, -0.2256878752776725616 ) ) ;
#9820=CARTESIAN_POINT ( 'NONE',  ( -0.6448876103708541807, -4.246476118072358474, -0.2256878752776773356 ) ) ;
#9824=AXIS2_PLACEMENT_3D ( 'NONE', #1839, #2564, #5070 ) ;
#9830=ORIENTED_EDGE ( 'NONE', *, *, #9539, .F. ) ;
#9831=CARTESIAN_POINT ( 'NONE',  ( 8.673617379884035472E-16, 4.618802153517012954, -5.000000000000000000 ) ) ;
#9832=EDGE_LOOP ( 'NONE', ( #3973, #2892, #1146, #5893, #8324 ) ) ;
#9837=APPLICATION_CONTEXT ( 'automotive_design' ) ;
#9867=DIRECTION ( 'NONE',  ( -1.000000000000000000, 0.000000000000000000, 0.000000000000000000 ) ) ;
#9872=AXIS2_PLACEMENT_3D ( 'NONE', #620, #4016, #5740 ) ;
#9875=CARTESIAN_POINT ( 'NONE',  ( -2.688821387764050996E-14, -4.618802153517012954, -0.4999999999999995559 ) ) ;
#9880=PRODUCT ( 'hex flange nut gradea_iso_ISO - 4161 - M5 - N', 'hex flange nut gradea_iso_ISO - 4161 - M5 - N', '', ( #1096 ) ) ;
#9909=CARTESIAN_POINT ( 'NONE',  ( 0.000000000000000000, 0.000000000000000000, -4.484454397937119197 ) ) ;
#9929=EDGE_CURVE ( 'NONE', #10561, #5966, #9612, .T. ) ;
#9936=ADVANCED_FACE ( 'NONE', ( #8979 ), #3118, .T. ) ;
#9948=CARTESIAN_POINT ( 'NONE',  ( 0.5469614295415388128, -4.303013824935362663, -3.535263753543555598 ) ) ;
#9953=ORIENTED_EDGE ( 'NONE', *, *, #7491, .F. ) ;
#9959=CONICAL_SURFACE ( 'NONE', #4287, 4.000000000000000000, 0.8911886515913786111 ) ;
#9973=CARTESIAN_POINT ( 'NONE',  ( -2.100000000000000089, 2.571758278209441957E-16, -5.000000000000000000 ) ) ;
#9976=CARTESIAN_POINT ( 'NONE',  ( 4.000000000000000888, -0.8578082829538523635, -3.433262215449808696 ) ) ;
#9980=CARTESIAN_POINT ( 'NONE',  ( -2.100000000000000089, 2.571758278209441957E-16, -0.2800830152838844622 ) ) ;
#9986=ORIENTED_EDGE ( 'NONE', *, *, #6882, .T. ) ;
#10002=LINE ( 'NONE', #7391, #10438 ) ;
#10037=AXIS2_PLACEMENT_3D ( 'NONE', #2709, #7820, #6978 ) ;
#10048=CARTESIAN_POINT ( 'NONE',  ( 0.000000000000000000, 0.000000000000000000, -5.000000000000000000 ) ) ;
#10055=EDGE_LOOP ( 'NONE', ( #9830, #5631, #2145, #5993, #4690 ) ) ;
#10077=DIRECTION ( 'NONE',  ( -0.000000000000000000, -0.000000000000000000, 1.000000000000000000 ) ) ;
#10092=COLOUR_RGB ( '', 0.09019608, 0.27058824, 0.51372549) ;
#10107=DIRECTION ( 'NONE',  ( -0.000000000000000000, -0.000000000000000000, 1.000000000000000000 ) ) ;
#10108=ORIENTED_EDGE ( 'NONE', *, *, #3715, .F. ) ;
#10113=CARTESIAN_POINT ( 'NONE',  ( -4.000000000000000000, 0.1981133338132459731, 2.096406544454392723E-17 ) ) ;
#10120=DIRECTION ( 'NONE',  ( -0.000000000000000000, -0.000000000000000000, 1.000000000000000000 ) ) ;
#10130=CARTESIAN_POINT ( 'NONE',  ( 0.000000000000000000, 0.000000000000000000, 3.469446951953614189E-15 ) ) ;
#10138=DIRECTION ( 'NONE',  ( 0.8660254037844379305, 0.5000000000000013323, 0.000000000000000000 ) ) ;
#10148=CARTESIAN_POINT ( 'NONE',  ( 4.000000000000000000, 2.309401076758515803, -0.4999999999999995559 ) ) ;
#10176=DIRECTION ( 'NONE',  ( 0.000000000000000000, 0.000000000000000000, -1.000000000000000000 ) ) ;
#10192=DIRECTION ( 'NONE',  ( 0.5000000000000013323, -0.8660254037844379305, 0.000000000000000000 ) ) ;
#10200=FACE_OUTER_BOUND ( 'NONE', #9832, .T. ) ;
#10213=CARTESIAN_POINT ( 'NONE',  ( 0.000000000000000000, 0.000000000000000000, -4.974599999999998801 ) ) ;
#10229=EDGE_CURVE ( 'NONE', #1419, #3831, #4550, .T. ) ;
#10239=ADVANCED_FACE ( 'NONE', ( #1511 ), #2775, .T. ) ;
#10267=DIRECTION ( 'NONE',  ( 1.000000000000000000, 0.000000000000000000, 0.000000000000000000 ) ) ;
#10272=B_SPLINE_CURVE_WITH_KNOTS ( 'NONE', 3,
 ( #8333, #9106, #2290, #10630, #3171, #2389 ),
 .UNSPECIFIED., .F., .F.,
 ( 4, 2, 4 ),
 ( 0.003358874760055551890, 0.004541967308452098118, 0.005725059856848645212 ),
 .UNSPECIFIED. ) ;
#10277=CARTESIAN_POINT ( 'NONE',  ( 0.6920835326022565237, 4.454600218803884459, -3.597382984111579862 ) ) ;
#10309=CARTESIAN_POINT ( 'NONE',  ( 2.756197834950227410, 3.027510591568626896, -3.223146290109805356 ) ) ;
#10315=CYLINDRICAL_SURFACE ( 'NONE', #1035, 2.100000000000000089 ) ;
#10325=EDGE_LOOP ( 'NONE', ( #2506, #2009, #5014, #9697 ) ) ;
#10337=CARTESIAN_POINT ( 'NONE',  ( 2.500000000000000888, 3.061616997868384127E-16, -4.974599999999998801 ) ) ;
#10378=FACE_OUTER_BOUND ( 'NONE', #10055, .T. ) ;
#10385=FACE_OUTER_BOUND ( 'NONE', #7849, .T. ) ;
#10403=B_SPLINE_CURVE_WITH_KNOTS ( 'NONE', 3,
 ( #1998, #5446, #4779, #6216, #8834 ),
 .UNSPECIFIED., .F., .F.,
 ( 4, 1, 4 ),
 ( 0.000000000000000000, 0.002309401076758505356, 0.004618802153517010713 ),
 .UNSPECIFIED. ) ;
#10404=AXIS2_PLACEMENT_3D ( 'NONE', #10130, #4918, #6564 ) ;
#10410=EDGE_CURVE ( 'NONE', #7320, #3058, #4902, .T. ) ;
#10415=DIRECTION ( 'NONE',  ( -0.000000000000000000, -0.000000000000000000, 1.000000000000000000 ) ) ;
#10419=DIRECTION ( 'NONE',  ( 0.000000000000000000, 0.000000000000000000, 1.000000000000000000 ) ) ;
#10420=CARTESIAN_POINT ( 'NONE',  ( 4.211140560182196957, -2.431303136016555122, -3.745885042887436622 ) ) ;
#10438=VECTOR ( 'NONE', #3282, 1000.000000000000114 ) ;
#10442=DIRECTION ( 'NONE',  ( 0.000000000000000000, 0.000000000000000000, 1.000000000000000000 ) ) ;
#10444=CARTESIAN_POINT ( 'NONE',  ( 2.059999999999998721, 0.000000000000000000, -0.3080913168122742518 ) ) ;
#10458=EDGE_LOOP ( 'NONE', ( #2032, #6793, #756, #8599 ) ) ;
#10473=ADVANCED_FACE ( 'NONE', ( #2909 ), #3789, .F. ) ;
#10475=DIRECTION ( 'NONE',  ( -1.000000000000000000, 0.000000000000000000, 0.000000000000000000 ) ) ;
#10481=VERTEX_POINT ( 'NONE', #7013 ) ;
#10520=CARTESIAN_POINT ( 'NONE',  ( -3.355112389629170799, 2.681727112203152963, -0.2256878752776689534 ) ) ;
#10522=ORIENTED_EDGE ( 'NONE', *, *, #2687, .T. ) ;
#10531=DIRECTION ( 'NONE',  ( -1.000000000000000000, 0.000000000000000000, 0.000000000000000000 ) ) ;
#10541=CARTESIAN_POINT ( 'NONE',  ( -3.436319922987618902, 2.634841920961291439, -3.531542292955721862 ) ) ;
#10561=VERTEX_POINT ( 'NONE', #8014 ) ;
#10596=CARTESIAN_POINT ( 'NONE',  ( -4.000000000000000000, -0.7890432684750890990, -0.04868663549882315533 ) ) ;
#10597=CARTESIAN_POINT ( 'NONE',  ( 0.1404048886732821022, 4.699864953788070565, -3.686887068327037387 ) ) ;
#10602=MECHANICAL_DESIGN_GEOMETRIC_PRESENTATION_REPRESENTATION('',(#7393),#6152);
#10630=CARTESIAN_POINT ( 'NONE',  ( 3.999999999999999112, -0.7890432684750902093, -0.04868663549882291247 ) ) ;
#10637=DIRECTION ( 'NONE',  ( -0.000000000000000000, -0.000000000000000000, 1.000000000000000000 ) ) ;
#10640=EDGE_CURVE ( 'NONE', #4773, #10561, #430, .T. ) ;
#10642=CARTESIAN_POINT ( 'NONE',  ( 4.000000000000000000, 2.309401076758515803, -0.4999999999999995559 ) ) ;
#10646=CARTESIAN_POINT ( 'NONE',  ( 4.000000000000000000, 2.309401076758515803, -0.4999999999999995559 ) ) ;
#10654=CARTESIAN_POINT ( 'NONE',  ( -0.5636800770129166693, -4.293361309317430319, -3.531542292955206275 ) ) ;
#10669=CIRCLE ( 'NONE', #9064, 0.5155456020628804703 ) ;
#10674=TOROIDAL_SURFACE ( 'NONE', #9786, 5.384454397937118664, 0.5155456020628804703 ) ;
#10681=DIRECTION ( 'NONE',  ( -0.000000000000000000, -0.000000000000000000, 1.000000000000000000 ) ) ;
#10688=ADVANCED_FACE ( 'NONE', ( #1400 ), #1874, .F. ) ;
#10700=CARTESIAN_POINT ( 'NONE',  ( -4.140404888673278272, -2.228338276487456415, -3.686887068327035166 ) ) ;
#10711=EDGE_CURVE ( 'NONE', #4045, #990, #2574, .T. ) ;
#10751=CARTESIAN_POINT ( 'NONE',  ( -4.000000000000000000, 2.309401076758498483, -0.4999999999999927280 ) ) ;
#10767=ADVANCED_BREP_SHAPE_REPRESENTATION ( '', ( #5578, #308 ), #6687 ) ;
#10772=CARTESIAN_POINT ( 'NONE',  ( 1.567478505476134606E-15, 4.618802153517012066, -5.000000000000000000 ) ) ;
#10778=CARTESIAN_POINT ( 'NONE',  ( 4.175648173966055587, -2.207990556236547608, -3.469390959564065291 ) ) ;
#10787=ORIENTED_EDGE ( 'NONE', *, *, #9399, .F. ) ;
#10792=AXIS2_PLACEMENT_3D ( 'NONE', #7675, #5125, #4285 ) ;
#10798=FACE_OUTER_BOUND ( 'NONE', #3619, .T. ) ;
#10800=ORIENTED_EDGE ( 'NONE', *, *, #9192, .T. ) ;
#10806=LINE ( 'NONE', #9973, #6941 ) ;
#10825=FACE_OUTER_BOUND ( 'NONE', #6245, .T. ) ;
#10855=FACE_OUTER_BOUND ( 'NONE', #1688, .T. ) ;
#10907=VERTEX_POINT ( 'NONE', #10420 ) ;
#10913=AXIS2_PLACEMENT_3D ( 'NONE', #4706, #8242, #6412 ) ;
#10921=EDGE_LOOP ( 'NONE', ( #987, #2792, #4117, #3986, #4611 ) ) ;
#10945=B_SPLINE_CURVE_WITH_KNOTS ( 'NONE', 3,
 ( #1768, #1819, #5103, #976, #2485 ),
 .UNSPECIFIED., .F., .F.,
 ( 4, 1, 4 ),
 ( 0.000000000000000000, 0.002309401076758506657, 0.004618802153517013315 ),
 .UNSPECIFIED. ) ;
#10951=AXIS2_PLACEMENT_3D ( 'NONE', #5484, #2873, #9583 ) ;
#10954=ORIENTED_EDGE ( 'NONE', *, *, #572, .F. ) ;
#10976=APPLICATION_CONTEXT ( 'automotive_design' ) ;
#10981=DIRECTION ( 'NONE',  ( -0.000000000000000000, 0.000000000000000000, -1.000000000000000000 ) ) ;
#10993=ORIENTED_EDGE ( 'NONE', *, *, #2144, .F. ) ;
ENDSEC;
END-ISO-10303-21;
